ISO-10303-21;
HEADER;
/* Generated by software containing ST-Developer
 * from STEP Tools, Inc. (www.steptools.com) 
 */

FILE_DESCRIPTION(
/* description */ ('Compact handwheel screw vise'),
/* implementation_level */ '2;1');

FILE_NAME(
/* name */ 'Flanged lead nut.step',
/* time_stamp */ '2026-10-29T16:08:22-07:00',
/* author */ (''),
/* organization */ (''),
/* preprocessor_version */ 'ST-DEVELOPER v20.2',
/* originating_system */ 'Autodesk Translation Framework v15.17.0.0',
/* authorisation */ '');

FILE_SCHEMA (('AUTOMOTIVE_DESIGN { 1 0 10303 214 3 1 1 }'));
ENDSEC;

DATA;
#10=MECHANICAL_DESIGN_GEOMETRIC_PRESENTATION_REPRESENTATION('',(#667),#25074);
#11=B_SPLINE_SURFACE_WITH_KNOTS('',3,3,((#13564,#13565,#13566,#13567,#13568,
#13569,#13570,#13571,#13572,#13573,#13574,#13575,#13576,#13577,#13578,#13579,
#13580,#13581,#13582,#13583,#13584,#13585,#13586,#13587,#13588,#13589,#13590,
#13591,#13592,#13593,#13594,#13595,#13596,#13597,#13598,#13599,#13600,#13601,
#13602,#13603,#13604,#13605,#13606,#13607,#13608,#13609,#13610,#13611,#13612,
#13613,#13614,#13615,#13616,#13617,#13618,#13619,#13620,#13621,#13622,#13623,
#13624,#13625,#13626,#13627,#13628,#13629,#13630,#13631,#13632,#13633,#13634,
#13635,#13636,#13637,#13638,#13639,#13640,#13641,#13642,#13643,#13644,#13645,
#13646,#13647,#13648,#13649,#13650,#13651,#13652,#13653,#13654,#13655,#13656,
#13657,#13658,#13659,#13660,#13661,#13662,#13663,#13664,#13665,#13666,#13667,
#13668,#13669,#13670,#13671,#13672,#13673,#13674,#13675,#13676,#13677,#13678),
(#13679,#13680,#13681,#13682,#13683,#13684,#13685,#13686,#13687,#13688,
#13689,#13690,#13691,#13692,#13693,#13694,#13695,#13696,#13697,#13698,#13699,
#13700,#13701,#13702,#13703,#13704,#13705,#13706,#13707,#13708,#13709,#13710,
#13711,#13712,#13713,#13714,#13715,#13716,#13717,#13718,#13719,#13720,#13721,
#13722,#13723,#13724,#13725,#13726,#13727,#13728,#13729,#13730,#13731,#13732,
#13733,#13734,#13735,#13736,#13737,#13738,#13739,#13740,#13741,#13742,#13743,
#13744,#13745,#13746,#13747,#13748,#13749,#13750,#13751,#13752,#13753,#13754,
#13755,#13756,#13757,#13758,#13759,#13760,#13761,#13762,#13763,#13764,#13765,
#13766,#13767,#13768,#13769,#13770,#13771,#13772,#13773,#13774,#13775,#13776,
#13777,#13778,#13779,#13780,#13781,#13782,#13783,#13784,#13785,#13786,#13787,
#13788,#13789,#13790,#13791,#13792,#13793),(#13794,#13795,#13796,#13797,
#13798,#13799,#13800,#13801,#13802,#13803,#13804,#13805,#13806,#13807,#13808,
#13809,#13810,#13811,#13812,#13813,#13814,#13815,#13816,#13817,#13818,#13819,
#13820,#13821,#13822,#13823,#13824,#13825,#13826,#13827,#13828,#13829,#13830,
#13831,#13832,#13833,#13834,#13835,#13836,#13837,#13838,#13839,#13840,#13841,
#13842,#13843,#13844,#13845,#13846,#13847,#13848,#13849,#13850,#13851,#13852,
#13853,#13854,#13855,#13856,#13857,#13858,#13859,#13860,#13861,#13862,#13863,
#13864,#13865,#13866,#13867,#13868,#13869,#13870,#13871,#13872,#13873,#13874,
#13875,#13876,#13877,#13878,#13879,#13880,#13881,#13882,#13883,#13884,#13885,
#13886,#13887,#13888,#13889,#13890,#13891,#13892,#13893,#13894,#13895,#13896,
#13897,#13898,#13899,#13900,#13901,#13902,#13903,#13904,#13905,#13906,#13907,
#13908),(#13909,#13910,#13911,#13912,#13913,#13914,#13915,#13916,#13917,
#13918,#13919,#13920,#13921,#13922,#13923,#13924,#13925,#13926,#13927,#13928,
#13929,#13930,#13931,#13932,#13933,#13934,#13935,#13936,#13937,#13938,#13939,
#13940,#13941,#13942,#13943,#13944,#13945,#13946,#13947,#13948,#13949,#13950,
#13951,#13952,#13953,#13954,#13955,#13956,#13957,#13958,#13959,#13960,#13961,
#13962,#13963,#13964,#13965,#13966,#13967,#13968,#13969,#13970,#13971,#13972,
#13973,#13974,#13975,#13976,#13977,#13978,#13979,#13980,#13981,#13982,#13983,
#13984,#13985,#13986,#13987,#13988,#13989,#13990,#13991,#13992,#13993,#13994,
#13995,#13996,#13997,#13998,#13999,#14000,#14001,#14002,#14003,#14004,#14005,
#14006,#14007,#14008,#14009,#14010,#14011,#14012,#14013,#14014,#14015,#14016,
#14017,#14018,#14019,#14020,#14021,#14022,#14023)),.UNSPECIFIED.,.F.,.F.,
 .F.,(4,4),(4,1,1,1,1,1,1,1,1,1,1,1,1,1,1,1,1,1,1,1,1,1,1,1,1,1,1,1,1,1,
1,1,1,1,1,1,1,1,1,1,1,1,1,1,1,1,1,1,1,1,1,1,1,1,1,1,1,1,1,1,1,1,1,1,1,1,
1,1,1,1,1,1,1,1,1,1,1,1,1,1,1,1,1,1,1,1,1,1,1,1,1,1,1,1,1,1,1,1,1,1,1,1,
1,1,1,1,1,1,1,1,1,1,4),(0.,0.173020531651036),(12.1475814751569,12.6421543672732,
13.1367272593894,13.6313001515056,14.1258730436219,14.6204459357381,15.1150188278544,
15.6095917199706,16.1041646120869,16.5987375042031,17.0933103963194,17.5878832884356,
18.0824561805519,18.5770290726681,19.0716019647843,19.5661748569006,20.0607477490168,
20.5553206411331,21.0498935332493,21.5444664253656,22.0390393174818,22.5336122095981,
23.0281851017143,23.5227579938306,24.0173308859468,24.511903778063,25.0064766701793,
25.5010495622955,25.9956224544118,26.490195346528,26.9847682386443,27.4793411307605,
27.9739140228768,28.468486914993,28.9630598071093,29.4576326992255,29.9522055913417,
30.446778483458,30.9413513755742,31.4359242676905,31.9304971598067,32.425070051923,
32.9196429440392,33.4142158361555,33.9087887282717,34.403361620388,34.8979345125042,
35.3925074046204,35.8870802967367,36.3816531888529,36.8762260809692,37.3707989730854,
37.8653718652017,38.3599447573179,38.8545176494342,39.3490905415504,39.8436634336667,
40.3382363257829,40.8328092178991,41.3273821100154,41.8219550021316,42.3165278942479,
42.8111007863641,43.3056736784804,43.8002465705966,44.2948194627129,44.7893923548291,
45.2839652469454,45.7785381390616,46.2731110311778,46.7676839232941,47.2622568154103,
47.7568297075266,48.2514025996428,48.7459754917591,49.2405483838753,49.7351212759916,
50.2296941681078,50.7242670602241,51.2188399523403,51.7134128444565,52.2079857365728,
52.702558628689,53.1971315208053,53.6917044129215,54.1862773050378,54.680850197154,
55.1754230892703,55.6699959813865,56.1645688735028,56.659141765619,57.1537146577353,
57.6482875498515,58.1428604419677,58.637433334084,59.1320062262002,59.6265791183165,
60.1211520104327,60.615724902549,61.1102977946652,61.6048706867815,62.0994435788977,
62.5940164710139,63.0885893631302,63.5831622552464,64.0777351473627,64.5723080394789,
65.0668809315952,65.5614538237114,66.0560267158277,66.5505996079439,67.0451725000601,
67.5397453921764),.UNSPECIFIED.);
#12=B_SPLINE_SURFACE_WITH_KNOTS('',3,3,((#14123,#14124,#14125,#14126,#14127,
#14128,#14129,#14130,#14131,#14132,#14133,#14134,#14135,#14136,#14137,#14138,
#14139,#14140,#14141,#14142,#14143,#14144,#14145,#14146,#14147,#14148,#14149,
#14150,#14151,#14152,#14153,#14154,#14155,#14156,#14157,#14158,#14159,#14160,
#14161,#14162,#14163,#14164,#14165,#14166,#14167,#14168,#14169,#14170,#14171,
#14172,#14173,#14174,#14175,#14176,#14177,#14178,#14179,#14180,#14181,#14182,
#14183,#14184,#14185,#14186,#14187,#14188,#14189,#14190,#14191,#14192,#14193,
#14194,#14195,#14196,#14197,#14198,#14199,#14200,#14201,#14202,#14203,#14204,
#14205,#14206,#14207,#14208,#14209,#14210,#14211,#14212,#14213,#14214,#14215,
#14216,#14217,#14218,#14219,#14220,#14221,#14222,#14223,#14224,#14225,#14226,
#14227,#14228,#14229,#14230,#14231,#14232,#14233,#14234,#14235,#14236,#14237),
(#14238,#14239,#14240,#14241,#14242,#14243,#14244,#14245,#14246,#14247,
#14248,#14249,#14250,#14251,#14252,#14253,#14254,#14255,#14256,#14257,#14258,
#14259,#14260,#14261,#14262,#14263,#14264,#14265,#14266,#14267,#14268,#14269,
#14270,#14271,#14272,#14273,#14274,#14275,#14276,#14277,#14278,#14279,#14280,
#14281,#14282,#14283,#14284,#14285,#14286,#14287,#14288,#14289,#14290,#14291,
#14292,#14293,#14294,#14295,#14296,#14297,#14298,#14299,#14300,#14301,#14302,
#14303,#14304,#14305,#14306,#14307,#14308,#14309,#14310,#14311,#14312,#14313,
#14314,#14315,#14316,#14317,#14318,#14319,#14320,#14321,#14322,#14323,#14324,
#14325,#14326,#14327,#14328,#14329,#14330,#14331,#14332,#14333,#14334,#14335,
#14336,#14337,#14338,#14339,#14340,#14341,#14342,#14343,#14344,#14345,#14346,
#14347,#14348,#14349,#14350,#14351,#14352),(#14353,#14354,#14355,#14356,
#14357,#14358,#14359,#14360,#14361,#14362,#14363,#14364,#14365,#14366,#14367,
#14368,#14369,#14370,#14371,#14372,#14373,#14374,#14375,#14376,#14377,#14378,
#14379,#14380,#14381,#14382,#14383,#14384,#14385,#14386,#14387,#14388,#14389,
#14390,#14391,#14392,#14393,#14394,#14395,#14396,#14397,#14398,#14399,#14400,
#14401,#14402,#14403,#14404,#14405,#14406,#14407,#14408,#14409,#14410,#14411,
#14412,#14413,#14414,#14415,#14416,#14417,#14418,#14419,#14420,#14421,#14422,
#14423,#14424,#14425,#14426,#14427,#14428,#14429,#14430,#14431,#14432,#14433,
#14434,#14435,#14436,#14437,#14438,#14439,#14440,#14441,#14442,#14443,#14444,
#14445,#14446,#14447,#14448,#14449,#14450,#14451,#14452,#14453,#14454,#14455,
#14456,#14457,#14458,#14459,#14460,#14461,#14462,#14463,#14464,#14465,#14466,
#14467),(#14468,#14469,#14470,#14471,#14472,#14473,#14474,#14475,#14476,
#14477,#14478,#14479,#14480,#14481,#14482,#14483,#14484,#14485,#14486,#14487,
#14488,#14489,#14490,#14491,#14492,#14493,#14494,#14495,#14496,#14497,#14498,
#14499,#14500,#14501,#14502,#14503,#14504,#14505,#14506,#14507,#14508,#14509,
#14510,#14511,#14512,#14513,#14514,#14515,#14516,#14517,#14518,#14519,#14520,
#14521,#14522,#14523,#14524,#14525,#14526,#14527,#14528,#14529,#14530,#14531,
#14532,#14533,#14534,#14535,#14536,#14537,#14538,#14539,#14540,#14541,#14542,
#14543,#14544,#14545,#14546,#14547,#14548,#14549,#14550,#14551,#14552,#14553,
#14554,#14555,#14556,#14557,#14558,#14559,#14560,#14561,#14562,#14563,#14564,
#14565,#14566,#14567,#14568,#14569,#14570,#14571,#14572,#14573,#14574,#14575,
#14576,#14577,#14578,#14579,#14580,#14581,#14582)),.UNSPECIFIED.,.F.,.F.,
 .F.,(4,4),(4,1,1,1,1,1,1,1,1,1,1,1,1,1,1,1,1,1,1,1,1,1,1,1,1,1,1,1,1,1,
1,1,1,1,1,1,1,1,1,1,1,1,1,1,1,1,1,1,1,1,1,1,1,1,1,1,1,1,1,1,1,1,1,1,1,1,
1,1,1,1,1,1,1,1,1,1,1,1,1,1,1,1,1,1,1,1,1,1,1,1,1,1,1,1,1,1,1,1,1,1,1,1,
1,1,1,1,1,1,1,1,1,1,4),(0.,0.173020531651036),(15.1888611523549,15.6834340444711,
16.1780069365874,16.6725798287036,17.1671527208199,17.6617256129361,18.1562985050523,
18.6508713971686,19.1454442892848,19.6400171814011,20.1345900735173,20.6291629656336,
21.1237358577498,21.6183087498661,22.1128816419823,22.6074545340986,23.1020274262148,
23.596600318331,24.0911732104473,24.5857461025635,25.0803189946798,25.574891886796,
26.0694647789123,26.5640376710285,27.0586105631448,27.553183455261,28.0477563473773,
28.5423292394935,29.0369021316097,29.531475023726,30.0260479158422,30.5206208079585,
31.0151937000747,31.509766592191,32.0043394843072,32.4989123764235,32.9934852685397,
33.488058160656,33.9826310527722,34.4772039448884,34.9717768370047,35.4663497291209,
35.9609226212372,36.4554955133534,36.9500684054697,37.4446412975859,37.9392141897022,
38.4337870818184,38.9283599739347,39.4229328660509,39.9175057581671,40.4120786502834,
40.9066515423996,41.4012244345159,41.8957973266321,42.3903702187484,42.8849431108646,
43.3795160029809,43.8740888950971,44.3686617872134,44.8632346793296,45.3578075714458,
45.8523804635621,46.3469533556783,46.8415262477946,47.3360991399108,47.8306720320271,
48.3252449241433,48.8198178162596,49.3143907083758,49.8089636004921,50.3035364926083,
50.7981093847245,51.2926822768408,51.787255168957,52.2818280610733,52.7764009531895,
53.2709738453058,53.765546737422,54.2601196295383,54.7546925216545,55.2492654137708,
55.743838305887,56.2384111980032,56.7329840901195,57.2275569822357,57.722129874352,
58.2167027664682,58.7112756585845,59.2058485507007,59.700421442817,60.1949943349332,
60.6895672270495,61.1841401191657,61.6787130112819,62.1732859033982,62.6678587955144,
63.1624316876307,63.6570045797469,64.1515774718632,64.6461503639794,65.1407232560957,
65.6352961482119,66.1298690403281,66.6244419324444,67.1190148245607,67.6135877166769,
68.1081606087931,68.6027335009094,69.0973063930256,69.5918792851419,70.0864521772581,
70.5810250693744),.UNSPECIFIED.);
#229=B_SPLINE_CURVE_WITH_KNOTS('',3,(#12520,#12521,#12522,#12523,#12524,
#12525,#12526,#12527,#12528,#12529,#12530,#12531,#12532,#12533,#12534,#12535,
#12536,#12537,#12538,#12539,#12540,#12541,#12542,#12543,#12544),
 .UNSPECIFIED.,.F.,.F.,(4,3,3,3,3,3,3,3,4),(-3.56038179279204,-3.46201024481372,
-2.96743735269747,-2.47286446058123,-1.97829156846498,-1.48371867634874,
-0.989145784232491,-0.494572892116246,0.),.UNSPECIFIED.);
#230=B_SPLINE_CURVE_WITH_KNOTS('',3,(#12547,#12548,#12549,#12550,#12551,
#12552,#12553,#12554,#12555,#12556,#12557,#12558,#12559,#12560,#12561,#12562,
#12563,#12564,#12565,#12566,#12567,#12568,#12569,#12570,#12571,#12572,#12573,
#12574,#12575,#12576,#12577,#12578,#12579,#12580,#12581,#12582,#12583,#12584,
#12585,#12586),.UNSPECIFIED.,.F.,.F.,(4,3,3,3,3,3,3,3,3,3,3,3,3,4),(0.937891254796418,
0.989145784232494,1.48371867634874,1.97829156846498,2.47286446058123,2.96743735269748,
3.46201024481372,3.95658313692997,4.45115602904621,4.94572892116246,5.44030181327871,
5.93487470539495,6.42944759751119,6.80228742277363),.UNSPECIFIED.);
#231=B_SPLINE_CURVE_WITH_KNOTS('',3,(#12591,#12592,#12593,#12594,#12595,
#12596,#12597,#12598,#12599,#12600,#12601,#12602,#12603,#12604,#12605,#12606,
#12607,#12608,#12609,#12610,#12611,#12612,#12613,#12614,#12615,#12616,#12617,
#12618,#12619,#12620,#12621,#12622,#12623,#12624,#12625,#12626,#12627,#12628,
#12629,#12630),.UNSPECIFIED.,.F.,.F.,(4,3,3,3,3,3,3,3,3,3,3,3,3,4),(-9.8435670999716,
-9.39688495020867,-8.90231205809242,-8.40773916597618,-7.91316627385993,
-7.41859338174369,-6.92402048962744,-6.42944759751119,-5.93487470539495,
-5.4403018132787,-4.94572892116246,-4.45115602904621,-3.95658313692996,
-3.56038179279204),.UNSPECIFIED.);
#232=B_SPLINE_CURVE_WITH_KNOTS('',3,(#12631,#12632,#12633,#12634,#12635,
#12636,#12637,#12638,#12639,#12640,#12641,#12642,#12643,#12644,#12645,#12646,
#12647,#12648,#12649,#12650,#12651,#12652,#12653,#12654,#12655,#12656,#12657,
#12658,#12659,#12660,#12661,#12662,#12663,#12664,#12665,#12666,#12667,#12668,
#12669,#12670,#12671,#12672,#12673),.UNSPECIFIED.,.F.,.F.,(4,3,3,3,3,3,
3,3,3,3,3,3,3,3,4),(6.80228742277363,6.92402048962744,7.41859338174369,
7.91316627385993,8.40773916597617,8.90231205809242,9.39688495020867,9.89145784232491,
10.3860307344412,10.8806036265574,11.3751765186736,11.8697494107899,12.3643223029061,
12.8588951950224,13.0854727299532),.UNSPECIFIED.);
#233=B_SPLINE_CURVE_WITH_KNOTS('',3,(#12678,#12679,#12680,#12681,#12682,
#12683,#12684,#12685,#12686,#12687,#12688,#12689,#12690,#12691,#12692,#12693,
#12694,#12695,#12696,#12697,#12698,#12699,#12700,#12701,#12702,#12703,#12704,
#12705,#12706,#12707,#12708,#12709,#12710,#12711,#12712,#12713,#12714,#12715,
#12716,#12717,#12718,#12719,#12720),.UNSPECIFIED.,.F.,.F.,(4,3,3,3,3,3,
3,3,3,3,3,3,3,3,4),(-16.1267524071512,-15.8263325477199,-15.3317596556036,
-14.8371867634874,-14.3426138713711,-13.8480409792549,-13.3534680871386,
-12.8588951950224,-12.3643223029061,-11.8697494107899,-11.3751765186736,
-10.8806036265574,-10.3860307344412,-9.89145784232491,-9.8435670999716),
 .UNSPECIFIED.);
#234=B_SPLINE_CURVE_WITH_KNOTS('',3,(#12721,#12722,#12723,#12724,#12725,
#12726,#12727,#12728,#12729,#12730,#12731,#12732,#12733,#12734,#12735,#12736,
#12737,#12738,#12739,#12740,#12741,#12742,#12743,#12744,#12745,#12746,#12747,
#12748,#12749,#12750,#12751,#12752,#12753,#12754,#12755,#12756,#12757,#12758,
#12759,#12760,#12761,#12762,#12763),.UNSPECIFIED.,.F.,.F.,(4,3,3,3,3,3,
3,3,3,3,3,3,3,3,4),(13.0854727299532,13.3534680871386,13.8480409792549,
14.3426138713711,14.8371867634874,15.3317596556036,15.8263325477199,16.3209054398361,
16.8154783319523,17.3100512240686,17.8046241161848,18.2991970083011,18.7937699004173,
19.2883427925336,19.3686580371328),.UNSPECIFIED.);
#235=B_SPLINE_CURVE_WITH_KNOTS('',3,(#12768,#12769,#12770,#12771,#12772,
#12773,#12774,#12775,#12776,#12777,#12778,#12779,#12780,#12781,#12782,#12783,
#12784,#12785,#12786,#12787,#12788,#12789,#12790,#12791,#12792,#12793,#12794,
#12795,#12796,#12797,#12798,#12799,#12800,#12801,#12802,#12803,#12804,#12805,
#12806,#12807,#12808,#12809,#12810),.UNSPECIFIED.,.F.,.F.,(4,3,3,3,3,3,
3,3,3,3,3,3,3,3,4),(-22.4099377143308,-22.2557801452311,-21.7612072531148,
-21.2666343609986,-20.7720614688823,-20.2774885767661,-19.7829156846498,
-19.2883427925336,-18.7937699004173,-18.2991970083011,-17.8046241161848,
-17.3100512240686,-16.8154783319523,-16.3209054398361,-16.1267524071512),
 .UNSPECIFIED.);
#236=B_SPLINE_CURVE_WITH_KNOTS('',3,(#12811,#12812,#12813,#12814,#12815,
#12816,#12817,#12818,#12819,#12820,#12821,#12822,#12823,#12824,#12825,#12826,
#12827,#12828,#12829,#12830,#12831,#12832,#12833,#12834,#12835,#12836,#12837,
#12838,#12839,#12840,#12841,#12842,#12843,#12844,#12845,#12846,#12847,#12848,
#12849,#12850),.UNSPECIFIED.,.F.,.F.,(4,3,3,3,3,3,3,3,3,3,3,3,3,4),(19.3686580371328,
19.7829156846498,20.2774885767661,20.7720614688823,21.2666343609986,21.7612072531148,
22.255780145231,22.7503530373473,23.2449259294635,23.7394988215798,24.234071713696,
24.7286446058123,25.2232174979285,25.6518433443124),.UNSPECIFIED.);
#237=B_SPLINE_CURVE_WITH_KNOTS('',3,(#12855,#12856,#12857,#12858,#12859,
#12860,#12861,#12862,#12863,#12864,#12865,#12866,#12867,#12868,#12869,#12870,
#12871,#12872,#12873,#12874,#12875,#12876,#12877,#12878,#12879,#12880,#12881,
#12882,#12883,#12884,#12885,#12886,#12887,#12888,#12889,#12890,#12891,#12892,
#12893,#12894,#12895,#12896,#12897),.UNSPECIFIED.,.F.,.F.,(4,3,3,3,3,3,
3,3,3,3,3,3,3,3,4),(-28.6931230215104,-28.6852277427422,-28.190654850626,
-27.6960819585097,-27.2015090663935,-26.7069361742773,-26.212363282161,
-25.7177903900448,-25.2232174979285,-24.7286446058123,-24.234071713696,
-23.7394988215798,-23.2449259294635,-22.7503530373473,-22.4099377143308),
 .UNSPECIFIED.);
#238=B_SPLINE_CURVE_WITH_KNOTS('',3,(#12898,#12899,#12900,#12901,#12902,
#12903,#12904,#12905,#12906,#12907,#12908,#12909,#12910,#12911,#12912,#12913,
#12914,#12915,#12916,#12917,#12918,#12919,#12920,#12921,#12922,#12923,#12924,
#12925,#12926,#12927,#12928,#12929,#12930,#12931,#12932,#12933,#12934,#12935,
#12936,#12937,#12938,#12939,#12940),.UNSPECIFIED.,.F.,.F.,(4,3,3,3,3,3,
3,3,3,3,3,3,3,3,4),(25.6518433443124,25.7177903900448,26.212363282161,26.7069361742773,
27.2015090663935,27.6960819585097,28.190654850626,28.6852277427422,29.1798006348585,
29.6743735269747,30.168946419091,30.6635193112072,31.1580922033235,31.6526650954397,
31.935028651492),.UNSPECIFIED.);
#239=B_SPLINE_CURVE_WITH_KNOTS('',3,(#12945,#12946,#12947,#12948,#12949,
#12950,#12951,#12952,#12953,#12954,#12955,#12956,#12957,#12958,#12959,#12960,
#12961,#12962,#12963,#12964,#12965,#12966,#12967,#12968,#12969,#12970,#12971,
#12972,#12973,#12974,#12975,#12976,#12977,#12978,#12979,#12980,#12981,#12982,
#12983,#12984),.UNSPECIFIED.,.F.,.F.,(4,3,3,3,3,3,3,3,3,3,3,3,3,4),(-34.97630832869,
-34.6201024481372,-34.1255295560209,-33.6309566639047,-33.1363837717884,
-32.6418108796722,-32.147237987556,-31.6526650954397,-31.1580922033235,
-30.6635193112072,-30.168946419091,-29.6743735269747,-29.1798006348585,
-28.6931230215104),.UNSPECIFIED.);
#240=B_SPLINE_CURVE_WITH_KNOTS('',3,(#12985,#12986,#12987,#12988,#12989,
#12990,#12991,#12992,#12993,#12994,#12995,#12996,#12997,#12998,#12999,#13000,
#13001,#13002,#13003,#13004,#13005,#13006,#13007,#13008,#13009,#13010,#13011,
#13012,#13013,#13014,#13015,#13016,#13017,#13018,#13019,#13020,#13021,#13022,
#13023,#13024,#13025,#13026,#13027),.UNSPECIFIED.,.F.,.F.,(4,3,3,3,3,3,
3,3,3,3,3,3,3,3,4),(31.935028651492,32.147237987556,32.6418108796722,33.1363837717885,
33.6309566639047,34.1255295560209,34.6201024481372,35.1146753402534,35.6092482323697,
36.1038211244859,36.5983940166022,37.0929669087184,37.5875398008347,38.0821126929509,
38.2182139586716),.UNSPECIFIED.);
#241=B_SPLINE_CURVE_WITH_KNOTS('',3,(#13032,#13033,#13034,#13035,#13036,
#13037,#13038,#13039,#13040,#13041,#13042,#13043,#13044,#13045,#13046,#13047,
#13048,#13049,#13050,#13051,#13052,#13053,#13054,#13055,#13056,#13057,#13058,
#13059,#13060,#13061,#13062,#13063,#13064,#13065,#13066,#13067,#13068,#13069,
#13070,#13071,#13072,#13073,#13074),.UNSPECIFIED.,.F.,.F.,(4,3,3,3,3,3,
3,3,3,3,3,3,3,3,4),(-41.2594936358696,-41.0495500456484,-40.5549771535321,
-40.0604042614159,-39.5658313692996,-39.0712584771834,-38.5766855850671,
-38.0821126929509,-37.5875398008347,-37.0929669087184,-36.5983940166022,
-36.1038211244859,-35.6092482323697,-35.1146753402534,-34.97630832869),
 .UNSPECIFIED.);
#242=B_SPLINE_CURVE_WITH_KNOTS('',3,(#13075,#13076,#13077,#13078,#13079,
#13080,#13081,#13082,#13083,#13084,#13085,#13086,#13087,#13088,#13089,#13090,
#13091,#13092,#13093,#13094,#13095,#13096,#13097,#13098,#13099,#13100,#13101,
#13102,#13103,#13104,#13105,#13106,#13107,#13108,#13109,#13110,#13111,#13112,
#13113,#13114),.UNSPECIFIED.,.F.,.F.,(4,3,3,3,3,3,3,3,3,3,3,3,3,4),(38.2182139586716,
38.5766855850671,39.0712584771834,39.5658313692996,40.0604042614159,40.5549771535321,
41.0495500456484,41.5441229377646,42.0386958298809,42.5332687219971,43.0278416141134,
43.5224145062296,44.0169873983459,44.5013992658512),.UNSPECIFIED.);
#243=B_SPLINE_CURVE_WITH_KNOTS('',3,(#13119,#13120,#13121,#13122,#13123,
#13124,#13125,#13126,#13127,#13128,#13129,#13130,#13131,#13132,#13133,#13134,
#13135,#13136,#13137,#13138,#13139,#13140,#13141,#13142,#13143,#13144,#13145,
#13146,#13147,#13148,#13149,#13150,#13151,#13152,#13153,#13154,#13155,#13156,
#13157,#13158,#13159,#13160,#13161),.UNSPECIFIED.,.F.,.F.,(4,3,3,3,3,3,
3,3,3,3,3,3,3,3,4),(-47.5426789430491,-47.4789976431596,-46.9844247510433,
-46.4898518589271,-45.9952789668108,-45.5007060746946,-45.0061331825783,
-44.5115602904621,-44.0169873983458,-43.5224145062296,-43.0278416141134,
-42.5332687219971,-42.0386958298809,-41.5441229377646,-41.2594936358696),
 .UNSPECIFIED.);
#244=B_SPLINE_CURVE_WITH_KNOTS('',3,(#13162,#13163,#13164,#13165,#13166,
#13167,#13168,#13169,#13170,#13171,#13172,#13173,#13174,#13175,#13176,#13177,
#13178,#13179,#13180,#13181,#13182,#13183,#13184,#13185,#13186,#13187,#13188,
#13189,#13190,#13191,#13192,#13193,#13194,#13195,#13196,#13197,#13198,#13199,
#13200,#13201,#13202,#13203,#13204),.UNSPECIFIED.,.F.,.F.,(4,3,3,3,3,3,
3,3,3,3,3,3,3,3,4),(44.5013992658512,44.5115602904621,45.0061331825783,
45.5007060746946,45.9952789668108,46.4898518589271,46.9844247510433,47.4789976431596,
47.9735705352758,48.4681434273921,48.9627163195083,49.4572892116245,49.9518621037408,
50.446434995857,50.7845845730308),.UNSPECIFIED.);
#245=B_SPLINE_CURVE_WITH_KNOTS('',3,(#13211,#13212,#13213,#13214,#13215,
#13216,#13217,#13218,#13219,#13220),.UNSPECIFIED.,.F.,.F.,(4,3,3,4),(-54.4542726622231,
-54.403018132787,-53.9084452406708,-53.8258642502287),.UNSPECIFIED.);
#246=B_SPLINE_CURVE_WITH_KNOTS('',3,(#13226,#13227,#13228,#13229,#13230,
#13231,#13232),.UNSPECIFIED.,.F.,.F.,(4,1,1,1,4),(65.9734457253856,66.0560267158277,
66.5505996079439,67.0451725000601,67.5397453921764),.UNSPECIFIED.);
#247=B_SPLINE_CURVE_WITH_KNOTS('',3,(#13235,#13236,#13237,#13238,#13239,
#13240,#13241,#13242,#13243,#13244,#13245,#13246),.UNSPECIFIED.,.F.,.F.,
(4,1,1,1,1,1,1,1,1,4),(65.9734457253856,66.1298690403281,66.6244419324444,
67.1190148245607,67.6135877166769,68.1081606087931,68.6027335009094,69.0973063930256,
69.5918792851419,69.643133814578),.UNSPECIFIED.);
#248=B_SPLINE_CURVE_WITH_KNOTS('',3,(#13251,#13252,#13253,#13254,#13255,
#13256,#13257,#13258,#13259,#13260,#13261,#13262,#13263,#13264,#13265,#13266),
 .UNSPECIFIED.,.F.,.F.,(4,1,1,1,1,1,1,1,1,1,1,1,1,4),(59.6902604182061,
60.1211520104327,60.615724902549,61.1102977946652,61.6048706867815,62.0994435788977,
62.5940164710139,63.0885893631302,63.5831622552464,64.0777351473627,64.5723080394789,
65.0668809315952,65.5614538237114,65.9734457253856),.UNSPECIFIED.);
#249=B_SPLINE_CURVE_WITH_KNOTS('',3,(#13267,#13268,#13269,#13270,#13271,
#13272,#13273,#13274,#13275,#13276,#13277,#13278,#13279,#13280,#13281,#13282,
#13283),.UNSPECIFIED.,.F.,.F.,(4,1,1,1,1,1,1,1,1,1,1,1,1,1,4),(59.6902604182061,
59.700421442817,60.1949943349332,60.6895672270495,61.1841401191657,61.6787130112819,
62.1732859033982,62.6678587955144,63.1624316876307,63.6570045797469,64.1515774718632,
64.6461503639794,65.1407232560957,65.6352961482119,65.9734457253856),
 .UNSPECIFIED.);
#250=B_SPLINE_CURVE_WITH_KNOTS('',3,(#13288,#13289,#13290,#13291,#13292,
#13293,#13294,#13295,#13296,#13297,#13298,#13299,#13300,#13301,#13302,#13303,
#13304),.UNSPECIFIED.,.F.,.F.,(4,1,1,1,1,1,1,1,1,1,1,1,1,1,4),(53.4070751110264,
53.6917044129215,54.1862773050378,54.680850197154,55.1754230892703,55.6699959813865,
56.1645688735028,56.659141765619,57.1537146577353,57.6482875498515,58.1428604419677,
58.637433334084,59.1320062262002,59.6265791183165,59.6902604182061),
 .UNSPECIFIED.);
#251=B_SPLINE_CURVE_WITH_KNOTS('',3,(#13305,#13306,#13307,#13308,#13309,
#13310,#13311,#13312,#13313,#13314,#13315,#13316,#13317,#13318,#13319,#13320),
 .UNSPECIFIED.,.F.,.F.,(4,1,1,1,1,1,1,1,1,1,1,1,1,4),(53.4070751110264,
53.765546737422,54.2601196295383,54.7546925216545,55.2492654137708,55.743838305887,
56.2384111980032,56.7329840901195,57.2275569822357,57.722129874352,58.2167027664682,
58.7112756585845,59.2058485507007,59.6902604182061),.UNSPECIFIED.);
#252=B_SPLINE_CURVE_WITH_KNOTS('',3,(#13325,#13326,#13327,#13328,#13329,
#13330,#13331,#13332,#13333,#13334,#13335,#13336,#13337,#13338,#13339,#13340,
#13341),.UNSPECIFIED.,.F.,.F.,(4,1,1,1,1,1,1,1,1,1,1,1,1,1,4),(47.1238898038469,
47.2622568154103,47.7568297075266,48.2514025996428,48.7459754917591,49.2405483838753,
49.7351212759916,50.2296941681078,50.7242670602241,51.2188399523403,51.7134128444565,
52.2079857365728,52.702558628689,53.1971315208053,53.4070751110264),
 .UNSPECIFIED.);
#253=B_SPLINE_CURVE_WITH_KNOTS('',3,(#13342,#13343,#13344,#13345,#13346,
#13347,#13348,#13349,#13350,#13351,#13352,#13353,#13354,#13355,#13356,#13357,
#13358),.UNSPECIFIED.,.F.,.F.,(4,1,1,1,1,1,1,1,1,1,1,1,1,1,4),(47.1238898038469,
47.3360991399108,47.8306720320271,48.3252449241433,48.8198178162596,49.3143907083758,
49.8089636004921,50.3035364926083,50.7981093847245,51.2926822768408,51.787255168957,
52.2818280610733,52.7764009531895,53.2709738453058,53.4070751110264),
 .UNSPECIFIED.);
#254=B_SPLINE_CURVE_WITH_KNOTS('',3,(#13363,#13364,#13365,#13366,#13367,
#13368,#13369,#13370,#13371,#13372,#13373,#13374,#13375,#13376,#13377,#13378),
 .UNSPECIFIED.,.F.,.F.,(4,1,1,1,1,1,1,1,1,1,1,1,1,4),(40.8407044966673,
41.3273821100154,41.8219550021316,42.3165278942479,42.8111007863641,43.3056736784804,
43.8002465705966,44.2948194627129,44.7893923548291,45.2839652469454,45.7785381390616,
46.2731110311778,46.7676839232941,47.1238898038469),.UNSPECIFIED.);
#255=B_SPLINE_CURVE_WITH_KNOTS('',3,(#13379,#13380,#13381,#13382,#13383,
#13384,#13385,#13386,#13387,#13388,#13389,#13390,#13391,#13392,#13393,#13394,
#13395),.UNSPECIFIED.,.F.,.F.,(4,1,1,1,1,1,1,1,1,1,1,1,1,1,4),(40.8407044966673,
40.9066515423996,41.4012244345159,41.8957973266321,42.3903702187484,42.8849431108646,
43.3795160029809,43.8740888950971,44.3686617872134,44.8632346793296,45.3578075714458,
45.8523804635621,46.3469533556783,46.8415262477946,47.1238898038469),
 .UNSPECIFIED.);
#256=B_SPLINE_CURVE_WITH_KNOTS('',3,(#13400,#13401,#13402,#13403,#13404,
#13405,#13406,#13407,#13408,#13409,#13410,#13411,#13412,#13413,#13414,#13415,
#13416),.UNSPECIFIED.,.F.,.F.,(4,1,1,1,1,1,1,1,1,1,1,1,1,1,4),(34.5575191894877,
34.8979345125042,35.3925074046204,35.8870802967367,36.3816531888529,36.8762260809692,
37.3707989730854,37.8653718652017,38.3599447573179,38.8545176494342,39.3490905415504,
39.8436634336667,40.3382363257829,40.8328092178991,40.8407044966673),
 .UNSPECIFIED.);
#257=B_SPLINE_CURVE_WITH_KNOTS('',3,(#13417,#13418,#13419,#13420,#13421,
#13422,#13423,#13424,#13425,#13426,#13427,#13428,#13429,#13430,#13431,#13432),
 .UNSPECIFIED.,.F.,.F.,(4,1,1,1,1,1,1,1,1,1,1,1,1,4),(34.5575191894877,
34.9717768370047,35.4663497291209,35.9609226212372,36.4554955133534,36.9500684054697,
37.4446412975859,37.9392141897022,38.4337870818184,38.9283599739347,39.4229328660509,
39.9175057581671,40.4120786502834,40.8407044966673),.UNSPECIFIED.);
#258=B_SPLINE_CURVE_WITH_KNOTS('',3,(#13437,#13438,#13439,#13440,#13441,
#13442,#13443,#13444,#13445,#13446,#13447,#13448,#13449,#13450,#13451,#13452,
#13453),.UNSPECIFIED.,.F.,.F.,(4,1,1,1,1,1,1,1,1,1,1,1,1,1,4),(28.2743338823081,
28.468486914993,28.9630598071093,29.4576326992255,29.9522055913417,30.446778483458,
30.9413513755742,31.4359242676905,31.9304971598067,32.425070051923,32.9196429440392,
33.4142158361555,33.9087887282717,34.403361620388,34.5575191894877),
 .UNSPECIFIED.);
#259=B_SPLINE_CURVE_WITH_KNOTS('',3,(#13454,#13455,#13456,#13457,#13458,
#13459,#13460,#13461,#13462,#13463,#13464,#13465,#13466,#13467,#13468,#13469,
#13470),.UNSPECIFIED.,.F.,.F.,(4,1,1,1,1,1,1,1,1,1,1,1,1,1,4),(28.2743338823081,
28.5423292394935,29.0369021316097,29.531475023726,30.0260479158422,30.5206208079585,
31.0151937000747,31.509766592191,32.0043394843072,32.4989123764235,32.9934852685397,
33.488058160656,33.9826310527722,34.4772039448884,34.5575191894877),
 .UNSPECIFIED.);
#260=B_SPLINE_CURVE_WITH_KNOTS('',3,(#13475,#13476,#13477,#13478,#13479,
#13480,#13481,#13482,#13483,#13484,#13485,#13486,#13487,#13488,#13489,#13490,
#13491),.UNSPECIFIED.,.F.,.F.,(4,1,1,1,1,1,1,1,1,1,1,1,1,1,4),(21.9911485751285,
22.0390393174818,22.5336122095981,23.0281851017143,23.5227579938306,24.0173308859468,
24.511903778063,25.0064766701793,25.5010495622955,25.9956224544118,26.490195346528,
26.9847682386443,27.4793411307605,27.9739140228768,28.2743338823081),
 .UNSPECIFIED.);
#261=B_SPLINE_CURVE_WITH_KNOTS('',3,(#13492,#13493,#13494,#13495,#13496,
#13497,#13498,#13499,#13500,#13501,#13502,#13503,#13504,#13505,#13506,#13507,
#13508),.UNSPECIFIED.,.F.,.F.,(4,1,1,1,1,1,1,1,1,1,1,1,1,1,4),(21.9911485751285,
22.1128816419823,22.6074545340986,23.1020274262148,23.596600318331,24.0911732104473,
24.5857461025635,25.0803189946798,25.574891886796,26.0694647789123,26.5640376710285,
27.0586105631448,27.553183455261,28.0477563473773,28.2743338823081),
 .UNSPECIFIED.);
#262=B_SPLINE_CURVE_WITH_KNOTS('',3,(#13514,#13515,#13516,#13517,#13518),
 .UNSPECIFIED.,.F.,.F.,(4,1,4),(15.1888611523549,15.6834340444711,15.7079632679489),
 .UNSPECIFIED.);
#263=B_SPLINE_CURVE_WITH_KNOTS('',3,(#13521,#13522,#13523,#13524,#13525,
#13526,#13527,#13528,#13529,#13530),.UNSPECIFIED.,.F.,.F.,(4,1,1,1,1,1,
1,4),(13.0854727299533,13.1367272593894,13.6313001515056,14.1258730436219,
14.6204459357381,15.1150188278544,15.6095917199706,15.7079632679489),
 .UNSPECIFIED.);
#264=B_SPLINE_CURVE_WITH_KNOTS('',3,(#13532,#13533,#13534,#13535,#13536,
#13537,#13538,#13539,#13540,#13541,#13542,#13543,#13544,#13545,#13546,#13547),
 .UNSPECIFIED.,.F.,.F.,(4,1,1,1,1,1,1,1,1,1,1,1,1,4),(15.7079632679489,
16.1041646120869,16.5987375042031,17.0933103963194,17.5878832884356,18.0824561805519,
18.5770290726681,19.0716019647843,19.5661748569006,20.0607477490168,20.5553206411331,
21.0498935332493,21.5444664253656,21.9911485751285),.UNSPECIFIED.);
#265=B_SPLINE_CURVE_WITH_KNOTS('',3,(#13548,#13549,#13550,#13551,#13552,
#13553,#13554,#13555,#13556,#13557,#13558,#13559,#13560,#13561,#13562,#13563),
 .UNSPECIFIED.,.F.,.F.,(4,1,1,1,1,1,1,1,1,1,1,1,1,4),(15.7079632679489,
16.1780069365874,16.6725798287036,17.1671527208199,17.6617256129361,18.1562985050523,
18.6508713971686,19.1454442892848,19.6400171814011,20.1345900735173,20.6291629656336,
21.1237358577498,21.6183087498661,21.9911485751285),.UNSPECIFIED.);
#266=B_SPLINE_CURVE_WITH_KNOTS('',3,(#14024,#14025,#14026,#14027,#14028,
#14029,#14030,#14031,#14032,#14033,#14034,#14035,#14036,#14037,#14038,#14039,
#14040,#14041,#14042,#14043,#14044,#14045,#14046,#14047,#14048,#14049,#14050,
#14051,#14052,#14053,#14054),.UNSPECIFIED.,.F.,.F.,(4,3,3,3,3,3,3,3,3,3,
4),(0.,0.0822466706468383,0.162608105240606,0.216579893838171,0.23924274204394,
0.301838371937517,0.36076250940623,0.388067588559334,0.409537377502954,
0.476290104322315,0.53753492181237),.UNSPECIFIED.);
#267=B_SPLINE_CURVE_WITH_KNOTS('',3,(#14055,#14056,#14057,#14058,#14059,
#14060,#14061,#14062,#14063,#14064,#14065,#14066,#14067,#14068,#14069,#14070,
#14071,#14072,#14073,#14074,#14075,#14076,#14077,#14078,#14079,#14080,#14081,
#14082),.UNSPECIFIED.,.F.,.F.,(4,3,3,3,3,3,3,3,3,4),(0.,0.0665230127441691,
0.13429495842692,0.176258819244205,0.195926107024299,0.263526952009386,
0.33682854572103,0.365338415901403,0.449700157257057,0.534061898612711),
 .UNSPECIFIED.);
#268=B_SPLINE_CURVE_WITH_KNOTS('',3,(#14083,#14084,#14085,#14086,#14087,
#14088,#14089,#14090,#14091,#14092,#14093,#14094,#14095,#14096,#14097,#14098,
#14099,#14100,#14101,#14102,#14103,#14104,#14105,#14106,#14107,#14108,#14109,
#14110,#14111,#14112,#14113,#14114,#14115,#14116,#14117,#14118,#14119,#14120,
#14121,#14122),.UNSPECIFIED.,.F.,.F.,(4,3,3,3,3,3,3,3,3,3,3,3,3,4),(-53.8258642502287,
-53.4138723485545,-52.9192994564383,-52.424726564322,-51.9301536722058,
-51.4355807800895,-50.9410078879733,-50.446434995857,-49.9518621037408,
-49.4572892116245,-48.9627163195083,-48.4681434273921,-47.9735705352758,
-47.5426789430491),.UNSPECIFIED.);
#269=B_SPLINE_CURVE_WITH_KNOTS('',3,(#14584,#14585,#14586,#14587,#14588,
#14589,#14590,#14591,#14592,#14593,#14594,#14595,#14596,#14597,#14598,#14599,
#14600,#14601,#14602,#14603,#14604,#14605,#14606,#14607,#14608,#14609,#14610,
#14611),.UNSPECIFIED.,.F.,.F.,(4,3,3,3,3,3,3,3,3,4),(0.,0.0665230199567328,
0.134294967830964,0.176258831509978,0.195926124443112,0.263526952009376,
0.336828549458816,0.365338416771381,0.449700157692121,0.534061898612861),
 .UNSPECIFIED.);
#270=B_SPLINE_CURVE_WITH_KNOTS('',3,(#14612,#14613,#14614,#14615,#14616,
#14617,#14618,#14619,#14620,#14621,#14622,#14623,#14624,#14625,#14626,#14627,
#14628,#14629,#14630,#14631,#14632,#14633,#14634,#14635,#14636,#14637,#14638,
#14639,#14640,#14641,#14642),.UNSPECIFIED.,.F.,.F.,(4,3,3,3,3,3,3,3,3,3,
4),(50.7845845730308,50.9410078879733,51.4355807800895,51.9301536722058,
52.424726564322,52.9192994564383,53.4138723485545,53.9084452406708,54.403018132787,
54.8975910249033,55.3921639170195),.UNSPECIFIED.);
#271=B_SPLINE_CURVE_WITH_KNOTS('',3,(#14643,#14644,#14645,#14646,#14647,
#14648,#14649,#14650,#14651,#14652,#14653,#14654,#14655,#14656,#14657,#14658,
#14659,#14660,#14661,#14662,#14663,#14664,#14665,#14666,#14667,#14668,#14669,
#14670,#14671,#14672,#14673),.UNSPECIFIED.,.F.,.F.,(4,3,3,3,3,3,3,3,3,3,
4),(0.,0.0822466663612967,0.162608100396307,0.216579890867136,0.239242742625966,
0.301838371937549,0.360762509406336,0.388067584071394,0.409537375230468,
0.476290092032249,0.537534921812695),.UNSPECIFIED.);
#603=SHAPE_REPRESENTATION_RELATIONSHIP('SRR','None',#25213,#631);
#631=ADVANCED_BREP_SHAPE_REPRESENTATION('',(#702),#25060);
#667=STYLED_ITEM('',(#25446),#702);
#702=MANIFOLD_SOLID_BREP('Body1',#8076);
#788=FACE_BOUND('',#1769,.T.);
#789=FACE_BOUND('',#1770,.T.);
#790=FACE_BOUND('',#1771,.T.);
#791=FACE_BOUND('',#1772,.T.);
#792=FACE_BOUND('',#1778,.T.);
#793=FACE_BOUND('',#1779,.T.);
#794=FACE_BOUND('',#1780,.T.);
#795=FACE_BOUND('',#1781,.T.);
#796=FACE_BOUND('',#1786,.T.);
#927=PLANE('',#8807);
#928=PLANE('',#8819);
#929=PLANE('',#8820);
#930=PLANE('',#8827);
#1201=FACE_OUTER_BOUND('',#1747,.T.);
#1202=FACE_OUTER_BOUND('',#1748,.T.);
#1203=FACE_OUTER_BOUND('',#1749,.T.);
#1204=FACE_OUTER_BOUND('',#1750,.T.);
#1205=FACE_OUTER_BOUND('',#1751,.T.);
#1206=FACE_OUTER_BOUND('',#1752,.T.);
#1207=FACE_OUTER_BOUND('',#1753,.T.);
#1208=FACE_OUTER_BOUND('',#1754,.T.);
#1209=FACE_OUTER_BOUND('',#1755,.T.);
#1210=FACE_OUTER_BOUND('',#1756,.T.);
#1211=FACE_OUTER_BOUND('',#1757,.T.);
#1212=FACE_OUTER_BOUND('',#1758,.T.);
#1213=FACE_OUTER_BOUND('',#1759,.T.);
#1214=FACE_OUTER_BOUND('',#1760,.T.);
#1215=FACE_OUTER_BOUND('',#1761,.T.);
#1216=FACE_OUTER_BOUND('',#1762,.T.);
#1217=FACE_OUTER_BOUND('',#1763,.T.);
#1218=FACE_OUTER_BOUND('',#1764,.T.);
#1219=FACE_OUTER_BOUND('',#1765,.T.);
#1220=FACE_OUTER_BOUND('',#1766,.T.);
#1221=FACE_OUTER_BOUND('',#1767,.T.);
#1222=FACE_OUTER_BOUND('',#1768,.T.);
#1223=FACE_OUTER_BOUND('',#1773,.T.);
#1224=FACE_OUTER_BOUND('',#1774,.T.);
#1225=FACE_OUTER_BOUND('',#1775,.T.);
#1226=FACE_OUTER_BOUND('',#1776,.T.);
#1227=FACE_OUTER_BOUND('',#1777,.T.);
#1228=FACE_OUTER_BOUND('',#1782,.T.);
#1229=FACE_OUTER_BOUND('',#1783,.T.);
#1230=FACE_OUTER_BOUND('',#1784,.T.);
#1231=FACE_OUTER_BOUND('',#1785,.T.);
#1747=EDGE_LOOP('',(#5923,#5924,#5925,#5926));
#1748=EDGE_LOOP('',(#5927,#5928,#5929,#5930));
#1749=EDGE_LOOP('',(#5931,#5932,#5933,#5934));
#1750=EDGE_LOOP('',(#5935,#5936,#5937,#5938));
#1751=EDGE_LOOP('',(#5939,#5940,#5941,#5942));
#1752=EDGE_LOOP('',(#5943,#5944,#5945,#5946));
#1753=EDGE_LOOP('',(#5947,#5948,#5949,#5950));
#1754=EDGE_LOOP('',(#5951,#5952,#5953,#5954));
#1755=EDGE_LOOP('',(#5955,#5956,#5957));
#1756=EDGE_LOOP('',(#5958,#5959,#5960,#5961));
#1757=EDGE_LOOP('',(#5962,#5963,#5964,#5965));
#1758=EDGE_LOOP('',(#5966,#5967,#5968,#5969));
#1759=EDGE_LOOP('',(#5970,#5971,#5972,#5973));
#1760=EDGE_LOOP('',(#5974,#5975,#5976,#5977));
#1761=EDGE_LOOP('',(#5978,#5979,#5980,#5981));
#1762=EDGE_LOOP('',(#5982,#5983,#5984,#5985));
#1763=EDGE_LOOP('',(#5986,#5987,#5988,#5989));
#1764=EDGE_LOOP('',(#5990,#5991,#5992,#5993));
#1765=EDGE_LOOP('',(#5994,#5995,#5996,#5997));
#1766=EDGE_LOOP('',(#5998,#5999,#6000,#6001,#6002,#6003,#6004,#6005,#6006,
#6007,#6008,#6009,#6010,#6011,#6012,#6013,#6014,#6015,#6016,#6017,#6018,
#6019));
#1767=EDGE_LOOP('',(#6020,#6021,#6022,#6023,#6024,#6025,#6026,#6027,#6028,
#6029,#6030,#6031,#6032,#6033,#6034,#6035,#6036,#6037,#6038,#6039,#6040));
#1768=EDGE_LOOP('',(#6041,#6042));
#1769=EDGE_LOOP('',(#6043,#6044,#6045,#6046,#6047));
#1770=EDGE_LOOP('',(#6048));
#1771=EDGE_LOOP('',(#6049));
#1772=EDGE_LOOP('',(#6050));
#1773=EDGE_LOOP('',(#6051,#6052,#6053,#6054));
#1774=EDGE_LOOP('',(#6055,#6056,#6057,#6058));
#1775=EDGE_LOOP('',(#6059,#6060,#6061,#6062));
#1776=EDGE_LOOP('',(#6063,#6064,#6065,#6066));
#1777=EDGE_LOOP('',(#6067,#6068));
#1778=EDGE_LOOP('',(#6069));
#1779=EDGE_LOOP('',(#6070));
#1780=EDGE_LOOP('',(#6071));
#1781=EDGE_LOOP('',(#6072));
#1782=EDGE_LOOP('',(#6073,#6074,#6075,#6076));
#1783=EDGE_LOOP('',(#6077,#6078,#6079,#6080,#6081));
#1784=EDGE_LOOP('',(#6082,#6083,#6084,#6085));
#1785=EDGE_LOOP('',(#6086));
#1786=EDGE_LOOP('',(#6087,#6088,#6089,#6090));
#2257=LINE('',#12518,#2765);
#2258=LINE('',#12590,#2766);
#2259=LINE('',#12677,#2767);
#2260=LINE('',#12767,#2768);
#2261=LINE('',#12854,#2769);
#2262=LINE('',#12944,#2770);
#2263=LINE('',#13031,#2771);
#2264=LINE('',#13118,#2772);
#2265=LINE('',#13208,#2773);
#2266=LINE('',#13224,#2774);
#2267=LINE('',#13250,#2775);
#2268=LINE('',#13287,#2776);
#2269=LINE('',#13324,#2777);
#2270=LINE('',#13362,#2778);
#2271=LINE('',#13399,#2779);
#2272=LINE('',#13436,#2780);
#2273=LINE('',#13474,#2781);
#2274=LINE('',#13512,#2782);
#2275=LINE('',#14677,#2783);
#2276=LINE('',#14689,#2784);
#2277=LINE('',#14693,#2785);
#2278=LINE('',#14697,#2786);
#2279=LINE('',#14701,#2787);
#2280=LINE('',#14702,#2788);
#2281=LINE('',#14703,#2789);
#2282=LINE('',#14712,#2790);
#2765=VECTOR('',#10167,0.45);
#2766=VECTOR('',#10172,0.45);
#2767=VECTOR('',#10175,0.45);
#2768=VECTOR('',#10178,0.45);
#2769=VECTOR('',#10181,0.45);
#2770=VECTOR('',#10184,0.45);
#2771=VECTOR('',#10187,0.45);
#2772=VECTOR('',#10190,0.45);
#2773=VECTOR('',#10193,0.45);
#2774=VECTOR('',#10198,0.625);
#2775=VECTOR('',#10203,0.625);
#2776=VECTOR('',#10206,0.625);
#2777=VECTOR('',#10209,0.625);
#2778=VECTOR('',#10212,0.625);
#2779=VECTOR('',#10215,0.625);
#2780=VECTOR('',#10218,0.625);
#2781=VECTOR('',#10221,0.625);
#2782=VECTOR('',#10224,0.625);
#2783=VECTOR('',#10231,1.);
#2784=VECTOR('',#10246,0.225);
#2785=VECTOR('',#10251,0.225);
#2786=VECTOR('',#10256,0.225);
#2787=VECTOR('',#10259,1.);
#2788=VECTOR('',#10260,1.);
#2789=VECTOR('',#10261,1.);
#2790=VECTOR('',#10274,1.1);
#3247=CIRCLE('',#8785,0.457875);
#3248=CIRCLE('',#8794,0.457875);
#3249=CIRCLE('',#8796,0.625);
#3250=CIRCLE('',#8805,0.625);
#3251=CIRCLE('',#8808,1.9);
#3252=CIRCLE('',#8809,0.457875);
#3253=CIRCLE('',#8810,0.225);
#3254=CIRCLE('',#8811,0.225);
#3255=CIRCLE('',#8812,0.225);
#3256=CIRCLE('',#8814,0.225);
#3257=CIRCLE('',#8816,0.225);
#3258=CIRCLE('',#8818,0.225);
#3259=CIRCLE('',#8821,1.9);
#3260=CIRCLE('',#8822,1.1);
#3261=CIRCLE('',#8826,1.1);
#3596=VERTEX_POINT('',#12516);
#3597=VERTEX_POINT('',#12517);
#3598=VERTEX_POINT('',#12519);
#3599=VERTEX_POINT('',#12545);
#3600=VERTEX_POINT('',#12588);
#3601=VERTEX_POINT('',#12589);
#3602=VERTEX_POINT('',#12675);
#3603=VERTEX_POINT('',#12676);
#3604=VERTEX_POINT('',#12765);
#3605=VERTEX_POINT('',#12766);
#3606=VERTEX_POINT('',#12852);
#3607=VERTEX_POINT('',#12853);
#3608=VERTEX_POINT('',#12942);
#3609=VERTEX_POINT('',#12943);
#3610=VERTEX_POINT('',#13029);
#3611=VERTEX_POINT('',#13030);
#3612=VERTEX_POINT('',#13116);
#3613=VERTEX_POINT('',#13117);
#3614=VERTEX_POINT('',#13206);
#3615=VERTEX_POINT('',#13207);
#3616=VERTEX_POINT('',#13209);
#3617=VERTEX_POINT('',#13222);
#3618=VERTEX_POINT('',#13223);
#3619=VERTEX_POINT('',#13225);
#3620=VERTEX_POINT('',#13233);
#3621=VERTEX_POINT('',#13248);
#3622=VERTEX_POINT('',#13249);
#3623=VERTEX_POINT('',#13285);
#3624=VERTEX_POINT('',#13286);
#3625=VERTEX_POINT('',#13322);
#3626=VERTEX_POINT('',#13323);
#3627=VERTEX_POINT('',#13360);
#3628=VERTEX_POINT('',#13361);
#3629=VERTEX_POINT('',#13397);
#3630=VERTEX_POINT('',#13398);
#3631=VERTEX_POINT('',#13434);
#3632=VERTEX_POINT('',#13435);
#3633=VERTEX_POINT('',#13472);
#3634=VERTEX_POINT('',#13473);
#3635=VERTEX_POINT('',#13510);
#3636=VERTEX_POINT('',#13511);
#3637=VERTEX_POINT('',#13513);
#3638=VERTEX_POINT('',#13519);
#3639=VERTEX_POINT('',#14583);
#3640=VERTEX_POINT('',#14675);
#3641=VERTEX_POINT('',#14676);
#3642=VERTEX_POINT('',#14680);
#3643=VERTEX_POINT('',#14682);
#3644=VERTEX_POINT('',#14684);
#3645=VERTEX_POINT('',#14687);
#3646=VERTEX_POINT('',#14691);
#3647=VERTEX_POINT('',#14695);
#3648=VERTEX_POINT('',#14699);
#3649=VERTEX_POINT('',#14700);
#3650=VERTEX_POINT('',#14706);
#3651=VERTEX_POINT('',#14711);
#4448=EDGE_CURVE('',#3596,#3597,#2257,.T.);
#4449=EDGE_CURVE('',#3597,#3598,#229,.T.);
#4450=EDGE_CURVE('',#3598,#3599,#3247,.F.);
#4451=EDGE_CURVE('',#3599,#3596,#230,.T.);
#4452=EDGE_CURVE('',#3600,#3601,#2258,.T.);
#4453=EDGE_CURVE('',#3601,#3597,#231,.T.);
#4454=EDGE_CURVE('',#3596,#3600,#232,.T.);
#4455=EDGE_CURVE('',#3602,#3603,#2259,.T.);
#4456=EDGE_CURVE('',#3603,#3601,#233,.T.);
#4457=EDGE_CURVE('',#3600,#3602,#234,.T.);
#4458=EDGE_CURVE('',#3604,#3605,#2260,.T.);
#4459=EDGE_CURVE('',#3605,#3603,#235,.T.);
#4460=EDGE_CURVE('',#3602,#3604,#236,.T.);
#4461=EDGE_CURVE('',#3606,#3607,#2261,.T.);
#4462=EDGE_CURVE('',#3607,#3605,#237,.T.);
#4463=EDGE_CURVE('',#3604,#3606,#238,.T.);
#4464=EDGE_CURVE('',#3608,#3609,#2262,.T.);
#4465=EDGE_CURVE('',#3609,#3607,#239,.T.);
#4466=EDGE_CURVE('',#3606,#3608,#240,.T.);
#4467=EDGE_CURVE('',#3610,#3611,#2263,.T.);
#4468=EDGE_CURVE('',#3611,#3609,#241,.T.);
#4469=EDGE_CURVE('',#3608,#3610,#242,.T.);
#4470=EDGE_CURVE('',#3612,#3613,#2264,.T.);
#4471=EDGE_CURVE('',#3613,#3611,#243,.T.);
#4472=EDGE_CURVE('',#3610,#3612,#244,.T.);
#4473=EDGE_CURVE('',#3614,#3615,#2265,.T.);
#4474=EDGE_CURVE('',#3616,#3614,#3248,.F.);
#4475=EDGE_CURVE('',#3616,#3615,#245,.T.);
#4476=EDGE_CURVE('',#3617,#3618,#2266,.T.);
#4477=EDGE_CURVE('',#3618,#3619,#246,.T.);
#4478=EDGE_CURVE('',#3620,#3619,#3249,.T.);
#4479=EDGE_CURVE('',#3617,#3620,#247,.T.);
#4480=EDGE_CURVE('',#3621,#3622,#2267,.T.);
#4481=EDGE_CURVE('',#3622,#3618,#248,.T.);
#4482=EDGE_CURVE('',#3621,#3617,#249,.T.);
#4483=EDGE_CURVE('',#3623,#3624,#2268,.T.);
#4484=EDGE_CURVE('',#3624,#3622,#250,.T.);
#4485=EDGE_CURVE('',#3623,#3621,#251,.T.);
#4486=EDGE_CURVE('',#3625,#3626,#2269,.T.);
#4487=EDGE_CURVE('',#3626,#3624,#252,.T.);
#4488=EDGE_CURVE('',#3625,#3623,#253,.T.);
#4489=EDGE_CURVE('',#3627,#3628,#2270,.T.);
#4490=EDGE_CURVE('',#3628,#3626,#254,.T.);
#4491=EDGE_CURVE('',#3627,#3625,#255,.T.);
#4492=EDGE_CURVE('',#3629,#3630,#2271,.T.);
#4493=EDGE_CURVE('',#3630,#3628,#256,.T.);
#4494=EDGE_CURVE('',#3629,#3627,#257,.T.);
#4495=EDGE_CURVE('',#3631,#3632,#2272,.T.);
#4496=EDGE_CURVE('',#3632,#3630,#258,.T.);
#4497=EDGE_CURVE('',#3631,#3629,#259,.T.);
#4498=EDGE_CURVE('',#3633,#3634,#2273,.T.);
#4499=EDGE_CURVE('',#3634,#3632,#260,.T.);
#4500=EDGE_CURVE('',#3633,#3631,#261,.T.);
#4501=EDGE_CURVE('',#3635,#3636,#2274,.T.);
#4502=EDGE_CURVE('',#3637,#3635,#262,.T.);
#4503=EDGE_CURVE('',#3638,#3637,#3250,.T.);
#4504=EDGE_CURVE('',#3638,#3636,#263,.T.);
#4505=EDGE_CURVE('',#3636,#3634,#264,.T.);
#4506=EDGE_CURVE('',#3635,#3633,#265,.T.);
#4507=EDGE_CURVE('',#3619,#3616,#266,.T.);
#4508=EDGE_CURVE('',#3598,#3638,#267,.T.);
#4509=EDGE_CURVE('',#3615,#3613,#268,.T.);
#4510=EDGE_CURVE('',#3639,#3620,#269,.T.);
#4511=EDGE_CURVE('',#3612,#3639,#270,.T.);
#4512=EDGE_CURVE('',#3637,#3599,#271,.T.);
#4513=EDGE_CURVE('',#3640,#3641,#2275,.T.);
#4514=EDGE_CURVE('',#3641,#3640,#3251,.T.);
#4515=EDGE_CURVE('',#3614,#3639,#3252,.F.);
#4516=EDGE_CURVE('',#3642,#3642,#3253,.T.);
#4517=EDGE_CURVE('',#3643,#3643,#3254,.T.);
#4518=EDGE_CURVE('',#3644,#3644,#3255,.T.);
#4519=EDGE_CURVE('',#3645,#3645,#3256,.T.);
#4520=EDGE_CURVE('',#3645,#3644,#2276,.T.);
#4521=EDGE_CURVE('',#3646,#3646,#3257,.T.);
#4522=EDGE_CURVE('',#3646,#3643,#2277,.T.);
#4523=EDGE_CURVE('',#3647,#3647,#3258,.T.);
#4524=EDGE_CURVE('',#3647,#3642,#2278,.T.);
#4525=EDGE_CURVE('',#3648,#3649,#2279,.T.);
#4526=EDGE_CURVE('',#3641,#3648,#2280,.T.);
#4527=EDGE_CURVE('',#3649,#3640,#2281,.T.);
#4528=EDGE_CURVE('',#3648,#3649,#3259,.T.);
#4529=EDGE_CURVE('',#3650,#3650,#3260,.T.);
#4530=EDGE_CURVE('',#3650,#3651,#2282,.T.);
#4531=EDGE_CURVE('',#3651,#3651,#3261,.T.);
#5923=ORIENTED_EDGE('',*,*,#4448,.T.);
#5924=ORIENTED_EDGE('',*,*,#4449,.T.);
#5925=ORIENTED_EDGE('',*,*,#4450,.T.);
#5926=ORIENTED_EDGE('',*,*,#4451,.T.);
#5927=ORIENTED_EDGE('',*,*,#4452,.T.);
#5928=ORIENTED_EDGE('',*,*,#4453,.T.);
#5929=ORIENTED_EDGE('',*,*,#4448,.F.);
#5930=ORIENTED_EDGE('',*,*,#4454,.T.);
#5931=ORIENTED_EDGE('',*,*,#4455,.T.);
#5932=ORIENTED_EDGE('',*,*,#4456,.T.);
#5933=ORIENTED_EDGE('',*,*,#4452,.F.);
#5934=ORIENTED_EDGE('',*,*,#4457,.T.);
#5935=ORIENTED_EDGE('',*,*,#4458,.T.);
#5936=ORIENTED_EDGE('',*,*,#4459,.T.);
#5937=ORIENTED_EDGE('',*,*,#4455,.F.);
#5938=ORIENTED_EDGE('',*,*,#4460,.T.);
#5939=ORIENTED_EDGE('',*,*,#4461,.T.);
#5940=ORIENTED_EDGE('',*,*,#4462,.T.);
#5941=ORIENTED_EDGE('',*,*,#4458,.F.);
#5942=ORIENTED_EDGE('',*,*,#4463,.T.);
#5943=ORIENTED_EDGE('',*,*,#4464,.T.);
#5944=ORIENTED_EDGE('',*,*,#4465,.T.);
#5945=ORIENTED_EDGE('',*,*,#4461,.F.);
#5946=ORIENTED_EDGE('',*,*,#4466,.T.);
#5947=ORIENTED_EDGE('',*,*,#4467,.T.);
#5948=ORIENTED_EDGE('',*,*,#4468,.T.);
#5949=ORIENTED_EDGE('',*,*,#4464,.F.);
#5950=ORIENTED_EDGE('',*,*,#4469,.T.);
#5951=ORIENTED_EDGE('',*,*,#4470,.T.);
#5952=ORIENTED_EDGE('',*,*,#4471,.T.);
#5953=ORIENTED_EDGE('',*,*,#4467,.F.);
#5954=ORIENTED_EDGE('',*,*,#4472,.T.);
#5955=ORIENTED_EDGE('',*,*,#4473,.F.);
#5956=ORIENTED_EDGE('',*,*,#4474,.F.);
#5957=ORIENTED_EDGE('',*,*,#4475,.T.);
#5958=ORIENTED_EDGE('',*,*,#4476,.T.);
#5959=ORIENTED_EDGE('',*,*,#4477,.T.);
#5960=ORIENTED_EDGE('',*,*,#4478,.F.);
#5961=ORIENTED_EDGE('',*,*,#4479,.F.);
#5962=ORIENTED_EDGE('',*,*,#4480,.T.);
#5963=ORIENTED_EDGE('',*,*,#4481,.T.);
#5964=ORIENTED_EDGE('',*,*,#4476,.F.);
#5965=ORIENTED_EDGE('',*,*,#4482,.F.);
#5966=ORIENTED_EDGE('',*,*,#4483,.T.);
#5967=ORIENTED_EDGE('',*,*,#4484,.T.);
#5968=ORIENTED_EDGE('',*,*,#4480,.F.);
#5969=ORIENTED_EDGE('',*,*,#4485,.F.);
#5970=ORIENTED_EDGE('',*,*,#4486,.T.);
#5971=ORIENTED_EDGE('',*,*,#4487,.T.);
#5972=ORIENTED_EDGE('',*,*,#4483,.F.);
#5973=ORIENTED_EDGE('',*,*,#4488,.F.);
#5974=ORIENTED_EDGE('',*,*,#4489,.T.);
#5975=ORIENTED_EDGE('',*,*,#4490,.T.);
#5976=ORIENTED_EDGE('',*,*,#4486,.F.);
#5977=ORIENTED_EDGE('',*,*,#4491,.F.);
#5978=ORIENTED_EDGE('',*,*,#4492,.T.);
#5979=ORIENTED_EDGE('',*,*,#4493,.T.);
#5980=ORIENTED_EDGE('',*,*,#4489,.F.);
#5981=ORIENTED_EDGE('',*,*,#4494,.F.);
#5982=ORIENTED_EDGE('',*,*,#4495,.T.);
#5983=ORIENTED_EDGE('',*,*,#4496,.T.);
#5984=ORIENTED_EDGE('',*,*,#4492,.F.);
#5985=ORIENTED_EDGE('',*,*,#4497,.F.);
#5986=ORIENTED_EDGE('',*,*,#4498,.T.);
#5987=ORIENTED_EDGE('',*,*,#4499,.T.);
#5988=ORIENTED_EDGE('',*,*,#4495,.F.);
#5989=ORIENTED_EDGE('',*,*,#4500,.F.);
#5990=ORIENTED_EDGE('',*,*,#4501,.F.);
#5991=ORIENTED_EDGE('',*,*,#4502,.F.);
#5992=ORIENTED_EDGE('',*,*,#4503,.F.);
#5993=ORIENTED_EDGE('',*,*,#4504,.T.);
#5994=ORIENTED_EDGE('',*,*,#4501,.T.);
#5995=ORIENTED_EDGE('',*,*,#4505,.T.);
#5996=ORIENTED_EDGE('',*,*,#4498,.F.);
#5997=ORIENTED_EDGE('',*,*,#4506,.F.);
#5998=ORIENTED_EDGE('',*,*,#4507,.F.);
#5999=ORIENTED_EDGE('',*,*,#4477,.F.);
#6000=ORIENTED_EDGE('',*,*,#4481,.F.);
#6001=ORIENTED_EDGE('',*,*,#4484,.F.);
#6002=ORIENTED_EDGE('',*,*,#4487,.F.);
#6003=ORIENTED_EDGE('',*,*,#4490,.F.);
#6004=ORIENTED_EDGE('',*,*,#4493,.F.);
#6005=ORIENTED_EDGE('',*,*,#4496,.F.);
#6006=ORIENTED_EDGE('',*,*,#4499,.F.);
#6007=ORIENTED_EDGE('',*,*,#4505,.F.);
#6008=ORIENTED_EDGE('',*,*,#4504,.F.);
#6009=ORIENTED_EDGE('',*,*,#4508,.F.);
#6010=ORIENTED_EDGE('',*,*,#4449,.F.);
#6011=ORIENTED_EDGE('',*,*,#4453,.F.);
#6012=ORIENTED_EDGE('',*,*,#4456,.F.);
#6013=ORIENTED_EDGE('',*,*,#4459,.F.);
#6014=ORIENTED_EDGE('',*,*,#4462,.F.);
#6015=ORIENTED_EDGE('',*,*,#4465,.F.);
#6016=ORIENTED_EDGE('',*,*,#4468,.F.);
#6017=ORIENTED_EDGE('',*,*,#4471,.F.);
#6018=ORIENTED_EDGE('',*,*,#4509,.F.);
#6019=ORIENTED_EDGE('',*,*,#4475,.F.);
#6020=ORIENTED_EDGE('',*,*,#4510,.F.);
#6021=ORIENTED_EDGE('',*,*,#4511,.F.);
#6022=ORIENTED_EDGE('',*,*,#4472,.F.);
#6023=ORIENTED_EDGE('',*,*,#4469,.F.);
#6024=ORIENTED_EDGE('',*,*,#4466,.F.);
#6025=ORIENTED_EDGE('',*,*,#4463,.F.);
#6026=ORIENTED_EDGE('',*,*,#4460,.F.);
#6027=ORIENTED_EDGE('',*,*,#4457,.F.);
#6028=ORIENTED_EDGE('',*,*,#4454,.F.);
#6029=ORIENTED_EDGE('',*,*,#4451,.F.);
#6030=ORIENTED_EDGE('',*,*,#4512,.F.);
#6031=ORIENTED_EDGE('',*,*,#4502,.T.);
#6032=ORIENTED_EDGE('',*,*,#4506,.T.);
#6033=ORIENTED_EDGE('',*,*,#4500,.T.);
#6034=ORIENTED_EDGE('',*,*,#4497,.T.);
#6035=ORIENTED_EDGE('',*,*,#4494,.T.);
#6036=ORIENTED_EDGE('',*,*,#4491,.T.);
#6037=ORIENTED_EDGE('',*,*,#4488,.T.);
#6038=ORIENTED_EDGE('',*,*,#4485,.T.);
#6039=ORIENTED_EDGE('',*,*,#4482,.T.);
#6040=ORIENTED_EDGE('',*,*,#4479,.T.);
#6041=ORIENTED_EDGE('',*,*,#4513,.T.);
#6042=ORIENTED_EDGE('',*,*,#4514,.T.);
#6043=ORIENTED_EDGE('',*,*,#4510,.T.);
#6044=ORIENTED_EDGE('',*,*,#4478,.T.);
#6045=ORIENTED_EDGE('',*,*,#4507,.T.);
#6046=ORIENTED_EDGE('',*,*,#4474,.T.);
#6047=ORIENTED_EDGE('',*,*,#4515,.T.);
#6048=ORIENTED_EDGE('',*,*,#4516,.T.);
#6049=ORIENTED_EDGE('',*,*,#4517,.T.);
#6050=ORIENTED_EDGE('',*,*,#4518,.T.);
#6051=ORIENTED_EDGE('',*,*,#4519,.F.);
#6052=ORIENTED_EDGE('',*,*,#4520,.T.);
#6053=ORIENTED_EDGE('',*,*,#4518,.F.);
#6054=ORIENTED_EDGE('',*,*,#4520,.F.);
#6055=ORIENTED_EDGE('',*,*,#4521,.F.);
#6056=ORIENTED_EDGE('',*,*,#4522,.T.);
#6057=ORIENTED_EDGE('',*,*,#4517,.F.);
#6058=ORIENTED_EDGE('',*,*,#4522,.F.);
#6059=ORIENTED_EDGE('',*,*,#4523,.F.);
#6060=ORIENTED_EDGE('',*,*,#4524,.T.);
#6061=ORIENTED_EDGE('',*,*,#4516,.F.);
#6062=ORIENTED_EDGE('',*,*,#4524,.F.);
#6063=ORIENTED_EDGE('',*,*,#4525,.F.);
#6064=ORIENTED_EDGE('',*,*,#4526,.F.);
#6065=ORIENTED_EDGE('',*,*,#4513,.F.);
#6066=ORIENTED_EDGE('',*,*,#4527,.F.);
#6067=ORIENTED_EDGE('',*,*,#4525,.T.);
#6068=ORIENTED_EDGE('',*,*,#4528,.F.);
#6069=ORIENTED_EDGE('',*,*,#4519,.T.);
#6070=ORIENTED_EDGE('',*,*,#4521,.T.);
#6071=ORIENTED_EDGE('',*,*,#4523,.T.);
#6072=ORIENTED_EDGE('',*,*,#4529,.T.);
#6073=ORIENTED_EDGE('',*,*,#4527,.T.);
#6074=ORIENTED_EDGE('',*,*,#4514,.F.);
#6075=ORIENTED_EDGE('',*,*,#4526,.T.);
#6076=ORIENTED_EDGE('',*,*,#4528,.T.);
#6077=ORIENTED_EDGE('',*,*,#4473,.T.);
#6078=ORIENTED_EDGE('',*,*,#4509,.T.);
#6079=ORIENTED_EDGE('',*,*,#4470,.F.);
#6080=ORIENTED_EDGE('',*,*,#4511,.T.);
#6081=ORIENTED_EDGE('',*,*,#4515,.F.);
#6082=ORIENTED_EDGE('',*,*,#4529,.F.);
#6083=ORIENTED_EDGE('',*,*,#4530,.T.);
#6084=ORIENTED_EDGE('',*,*,#4531,.T.);
#6085=ORIENTED_EDGE('',*,*,#4530,.F.);
#6086=ORIENTED_EDGE('',*,*,#4531,.F.);
#6087=ORIENTED_EDGE('',*,*,#4512,.T.);
#6088=ORIENTED_EDGE('',*,*,#4450,.F.);
#6089=ORIENTED_EDGE('',*,*,#4508,.T.);
#6090=ORIENTED_EDGE('',*,*,#4503,.T.);
#7404=CYLINDRICAL_SURFACE('',#8784,0.457875);
#7405=CYLINDRICAL_SURFACE('',#8786,0.457875);
#7406=CYLINDRICAL_SURFACE('',#8787,0.457875);
#7407=CYLINDRICAL_SURFACE('',#8788,0.457875);
#7408=CYLINDRICAL_SURFACE('',#8789,0.457875);
#7409=CYLINDRICAL_SURFACE('',#8790,0.457875);
#7410=CYLINDRICAL_SURFACE('',#8791,0.457875);
#7411=CYLINDRICAL_SURFACE('',#8792,0.457875);
#7412=CYLINDRICAL_SURFACE('',#8793,0.457875);
#7413=CYLINDRICAL_SURFACE('',#8795,0.625);
#7414=CYLINDRICAL_SURFACE('',#8797,0.625);
#7415=CYLINDRICAL_SURFACE('',#8798,0.625);
#7416=CYLINDRICAL_SURFACE('',#8799,0.625);
#7417=CYLINDRICAL_SURFACE('',#8800,0.625);
#7418=CYLINDRICAL_SURFACE('',#8801,0.625);
#7419=CYLINDRICAL_SURFACE('',#8802,0.625);
#7420=CYLINDRICAL_SURFACE('',#8803,0.625);
#7421=CYLINDRICAL_SURFACE('',#8804,0.625);
#7422=CYLINDRICAL_SURFACE('',#8806,0.625);
#7423=CYLINDRICAL_SURFACE('',#8813,0.225);
#7424=CYLINDRICAL_SURFACE('',#8815,0.225);
#7425=CYLINDRICAL_SURFACE('',#8817,0.225);
#7426=CYLINDRICAL_SURFACE('',#8823,1.9);
#7427=CYLINDRICAL_SURFACE('',#8824,0.457875);
#7428=CYLINDRICAL_SURFACE('',#8825,1.1);
#7771=ADVANCED_FACE('',(#1201),#7404,.F.);
#7772=ADVANCED_FACE('',(#1202),#7405,.F.);
#7773=ADVANCED_FACE('',(#1203),#7406,.F.);
#7774=ADVANCED_FACE('',(#1204),#7407,.F.);
#7775=ADVANCED_FACE('',(#1205),#7408,.F.);
#7776=ADVANCED_FACE('',(#1206),#7409,.F.);
#7777=ADVANCED_FACE('',(#1207),#7410,.F.);
#7778=ADVANCED_FACE('',(#1208),#7411,.F.);
#7779=ADVANCED_FACE('',(#1209),#7412,.F.);
#7780=ADVANCED_FACE('',(#1210),#7413,.F.);
#7781=ADVANCED_FACE('',(#1211),#7414,.F.);
#7782=ADVANCED_FACE('',(#1212),#7415,.F.);
#7783=ADVANCED_FACE('',(#1213),#7416,.F.);
#7784=ADVANCED_FACE('',(#1214),#7417,.F.);
#7785=ADVANCED_FACE('',(#1215),#7418,.F.);
#7786=ADVANCED_FACE('',(#1216),#7419,.F.);
#7787=ADVANCED_FACE('',(#1217),#7420,.F.);
#7788=ADVANCED_FACE('',(#1218),#7421,.F.);
#7789=ADVANCED_FACE('',(#1219),#7422,.F.);
#7790=ADVANCED_FACE('',(#1220),#11,.F.);
#7791=ADVANCED_FACE('',(#1221),#12,.F.);
#7792=ADVANCED_FACE('',(#1222,#788,#789,#790,#791),#927,.T.);
#7793=ADVANCED_FACE('',(#1223),#7423,.F.);
#7794=ADVANCED_FACE('',(#1224),#7424,.F.);
#7795=ADVANCED_FACE('',(#1225),#7425,.F.);
#7796=ADVANCED_FACE('',(#1226),#928,.F.);
#7797=ADVANCED_FACE('',(#1227,#792,#793,#794,#795),#929,.F.);
#7798=ADVANCED_FACE('',(#1228),#7426,.T.);
#7799=ADVANCED_FACE('',(#1229),#7427,.F.);
#7800=ADVANCED_FACE('',(#1230),#7428,.T.);
#7801=ADVANCED_FACE('',(#1231,#796),#930,.F.);
#8076=CLOSED_SHELL('',(#7771,#7772,#7773,#7774,#7775,#7776,#7777,#7778,
#7779,#7780,#7781,#7782,#7783,#7784,#7785,#7786,#7787,#7788,#7789,#7790,
#7791,#7792,#7793,#7794,#7795,#7796,#7797,#7798,#7799,#7800,#7801));
#8783=AXIS2_PLACEMENT_3D('',#12514,#10163,#10164);
#8784=AXIS2_PLACEMENT_3D('',#12515,#10165,#10166);
#8785=AXIS2_PLACEMENT_3D('',#12546,#10168,#10169);
#8786=AXIS2_PLACEMENT_3D('',#12587,#10170,#10171);
#8787=AXIS2_PLACEMENT_3D('',#12674,#10173,#10174);
#8788=AXIS2_PLACEMENT_3D('',#12764,#10176,#10177);
#8789=AXIS2_PLACEMENT_3D('',#12851,#10179,#10180);
#8790=AXIS2_PLACEMENT_3D('',#12941,#10182,#10183);
#8791=AXIS2_PLACEMENT_3D('',#13028,#10185,#10186);
#8792=AXIS2_PLACEMENT_3D('',#13115,#10188,#10189);
#8793=AXIS2_PLACEMENT_3D('',#13205,#10191,#10192);
#8794=AXIS2_PLACEMENT_3D('',#13210,#10194,#10195);
#8795=AXIS2_PLACEMENT_3D('',#13221,#10196,#10197);
#8796=AXIS2_PLACEMENT_3D('',#13234,#10199,#10200);
#8797=AXIS2_PLACEMENT_3D('',#13247,#10201,#10202);
#8798=AXIS2_PLACEMENT_3D('',#13284,#10204,#10205);
#8799=AXIS2_PLACEMENT_3D('',#13321,#10207,#10208);
#8800=AXIS2_PLACEMENT_3D('',#13359,#10210,#10211);
#8801=AXIS2_PLACEMENT_3D('',#13396,#10213,#10214);
#8802=AXIS2_PLACEMENT_3D('',#13433,#10216,#10217);
#8803=AXIS2_PLACEMENT_3D('',#13471,#10219,#10220);
#8804=AXIS2_PLACEMENT_3D('',#13509,#10222,#10223);
#8805=AXIS2_PLACEMENT_3D('',#13520,#10225,#10226);
#8806=AXIS2_PLACEMENT_3D('',#13531,#10227,#10228);
#8807=AXIS2_PLACEMENT_3D('',#14674,#10229,#10230);
#8808=AXIS2_PLACEMENT_3D('',#14678,#10232,#10233);
#8809=AXIS2_PLACEMENT_3D('',#14679,#10234,#10235);
#8810=AXIS2_PLACEMENT_3D('',#14681,#10236,#10237);
#8811=AXIS2_PLACEMENT_3D('',#14683,#10238,#10239);
#8812=AXIS2_PLACEMENT_3D('',#14685,#10240,#10241);
#8813=AXIS2_PLACEMENT_3D('',#14686,#10242,#10243);
#8814=AXIS2_PLACEMENT_3D('',#14688,#10244,#10245);
#8815=AXIS2_PLACEMENT_3D('',#14690,#10247,#10248);
#8816=AXIS2_PLACEMENT_3D('',#14692,#10249,#10250);
#8817=AXIS2_PLACEMENT_3D('',#14694,#10252,#10253);
#8818=AXIS2_PLACEMENT_3D('',#14696,#10254,#10255);
#8819=AXIS2_PLACEMENT_3D('',#14698,#10257,#10258);
#8820=AXIS2_PLACEMENT_3D('',#14704,#10262,#10263);
#8821=AXIS2_PLACEMENT_3D('',#14705,#10264,#10265);
#8822=AXIS2_PLACEMENT_3D('',#14707,#10266,#10267);
#8823=AXIS2_PLACEMENT_3D('',#14708,#10268,#10269);
#8824=AXIS2_PLACEMENT_3D('',#14709,#10270,#10271);
#8825=AXIS2_PLACEMENT_3D('',#14710,#10272,#10273);
#8826=AXIS2_PLACEMENT_3D('',#14713,#10275,#10276);
#8827=AXIS2_PLACEMENT_3D('',#14714,#10277,#10278);
#10163=DIRECTION('axis',(0.,0.,1.));
#10164=DIRECTION('refdir',(1.,0.,0.));
#10165=DIRECTION('center_axis',(1.,0.,0.));
#10166=DIRECTION('ref_axis',(0.,0.207879895528894,-0.978154358490978));
#10167=DIRECTION('',(-1.,0.,0.));
#10168=DIRECTION('center_axis',(1.,0.,0.));
#10169=DIRECTION('ref_axis',(0.,0.,-1.));
#10170=DIRECTION('center_axis',(1.,0.,0.));
#10171=DIRECTION('ref_axis',(0.,0.,-1.));
#10172=DIRECTION('',(-1.,0.,0.));
#10173=DIRECTION('center_axis',(1.,0.,0.));
#10174=DIRECTION('ref_axis',(0.,0.,-1.));
#10175=DIRECTION('',(-1.,0.,0.));
#10176=DIRECTION('center_axis',(1.,0.,0.));
#10177=DIRECTION('ref_axis',(0.,0.,-1.));
#10178=DIRECTION('',(-1.,0.,0.));
#10179=DIRECTION('center_axis',(1.,0.,0.));
#10180=DIRECTION('ref_axis',(0.,0.,-1.));
#10181=DIRECTION('',(-1.,0.,0.));
#10182=DIRECTION('center_axis',(1.,0.,0.));
#10183=DIRECTION('ref_axis',(0.,0.,-1.));
#10184=DIRECTION('',(-1.,0.,0.));
#10185=DIRECTION('center_axis',(1.,0.,0.));
#10186=DIRECTION('ref_axis',(0.,0.,-1.));
#10187=DIRECTION('',(-1.,0.,0.));
#10188=DIRECTION('center_axis',(1.,0.,0.));
#10189=DIRECTION('ref_axis',(0.,0.,-1.));
#10190=DIRECTION('',(-1.,0.,0.));
#10191=DIRECTION('center_axis',(1.,0.,0.));
#10192=DIRECTION('ref_axis',(0.,0.,-1.));
#10193=DIRECTION('',(-1.,0.,0.));
#10194=DIRECTION('center_axis',(1.,0.,0.));
#10195=DIRECTION('ref_axis',(0.,0.,-1.));
#10196=DIRECTION('center_axis',(1.,0.,0.));
#10197=DIRECTION('ref_axis',(0.,2.68771689099506E-14,-1.));
#10198=DIRECTION('',(1.,3.30650148539799E-30,-1.22464679914735E-16));
#10199=DIRECTION('center_axis',(-1.,0.,0.));
#10200=DIRECTION('ref_axis',(0.,2.68771689099506E-14,-1.));
#10201=DIRECTION('center_axis',(1.,0.,0.));
#10202=DIRECTION('ref_axis',(0.,2.68771689099506E-14,-1.));
#10203=DIRECTION('',(1.,3.30650148539799E-30,-1.22464679914735E-16));
#10204=DIRECTION('center_axis',(1.,0.,0.));
#10205=DIRECTION('ref_axis',(0.,2.68771689099506E-14,-1.));
#10206=DIRECTION('',(1.,3.30650148539799E-30,-1.22464679914735E-16));
#10207=DIRECTION('center_axis',(1.,0.,0.));
#10208=DIRECTION('ref_axis',(0.,2.68771689099506E-14,-1.));
#10209=DIRECTION('',(1.,3.30650148539799E-30,-1.22464679914735E-16));
#10210=DIRECTION('center_axis',(1.,0.,0.));
#10211=DIRECTION('ref_axis',(0.,2.68771689099506E-14,-1.));
#10212=DIRECTION('',(1.,3.30650148539799E-30,-1.22464679914735E-16));
#10213=DIRECTION('center_axis',(1.,0.,0.));
#10214=DIRECTION('ref_axis',(0.,2.68771689099506E-14,-1.));
#10215=DIRECTION('',(1.,3.30650148539799E-30,-1.22464679914735E-16));
#10216=DIRECTION('center_axis',(1.,0.,0.));
#10217=DIRECTION('ref_axis',(0.,2.68771689099506E-14,-1.));
#10218=DIRECTION('',(1.,3.30650148539799E-30,-1.22464679914735E-16));
#10219=DIRECTION('center_axis',(1.,0.,0.));
#10220=DIRECTION('ref_axis',(0.,2.68771689099506E-14,-1.));
#10221=DIRECTION('',(1.,3.30650148539799E-30,-1.22464679914735E-16));
#10222=DIRECTION('center_axis',(1.,0.,0.));
#10223=DIRECTION('ref_axis',(0.,2.68771689099506E-14,-1.));
#10224=DIRECTION('',(1.,3.30650148539799E-30,-1.22464679914735E-16));
#10225=DIRECTION('center_axis',(1.,0.,0.));
#10226=DIRECTION('ref_axis',(0.,2.68771689099506E-14,-1.));
#10227=DIRECTION('center_axis',(1.,0.,0.));
#10228=DIRECTION('ref_axis',(0.,2.68771689099506E-14,-1.));
#10229=DIRECTION('center_axis',(1.,0.,0.));
#10230=DIRECTION('ref_axis',(0.,0.,-1.));
#10231=DIRECTION('',(0.,1.,0.));
#10232=DIRECTION('center_axis',(1.,0.,0.));
#10233=DIRECTION('ref_axis',(0.,0.,-1.));
#10234=DIRECTION('center_axis',(1.,0.,0.));
#10235=DIRECTION('ref_axis',(0.,0.,-1.));
#10236=DIRECTION('center_axis',(-1.,0.,0.));
#10237=DIRECTION('ref_axis',(0.,0.,-1.));
#10238=DIRECTION('center_axis',(-1.,0.,0.));
#10239=DIRECTION('ref_axis',(0.,0.,-1.));
#10240=DIRECTION('center_axis',(-1.,0.,0.));
#10241=DIRECTION('ref_axis',(0.,0.,-1.));
#10242=DIRECTION('center_axis',(1.,0.,0.));
#10243=DIRECTION('ref_axis',(0.,0.,-1.));
#10244=DIRECTION('center_axis',(1.,0.,0.));
#10245=DIRECTION('ref_axis',(0.,0.,-1.));
#10246=DIRECTION('',(1.,0.,0.));
#10247=DIRECTION('center_axis',(1.,0.,0.));
#10248=DIRECTION('ref_axis',(0.,0.,-1.));
#10249=DIRECTION('center_axis',(1.,0.,0.));
#10250=DIRECTION('ref_axis',(0.,0.,-1.));
#10251=DIRECTION('',(1.,0.,0.));
#10252=DIRECTION('center_axis',(1.,0.,0.));
#10253=DIRECTION('ref_axis',(0.,0.,-1.));
#10254=DIRECTION('center_axis',(1.,0.,0.));
#10255=DIRECTION('ref_axis',(0.,0.,-1.));
#10256=DIRECTION('',(1.,0.,0.));
#10257=DIRECTION('center_axis',(0.,0.,1.));
#10258=DIRECTION('ref_axis',(0.,-1.,0.));
#10259=DIRECTION('',(0.,-1.,0.));
#10260=DIRECTION('',(-1.,0.,0.));
#10261=DIRECTION('',(1.,0.,0.));
#10262=DIRECTION('center_axis',(1.,0.,0.));
#10263=DIRECTION('ref_axis',(0.,0.,-1.));
#10264=DIRECTION('center_axis',(1.,0.,0.));
#10265=DIRECTION('ref_axis',(0.,0.,-1.));
#10266=DIRECTION('center_axis',(1.,0.,0.));
#10267=DIRECTION('ref_axis',(0.,0.,-1.));
#10268=DIRECTION('center_axis',(1.,0.,0.));
#10269=DIRECTION('ref_axis',(0.,-1.22464679914735E-16,1.));
#10270=DIRECTION('center_axis',(1.,0.,0.));
#10271=DIRECTION('ref_axis',(0.,0.,-1.));
#10272=DIRECTION('center_axis',(1.,0.,0.));
#10273=DIRECTION('ref_axis',(0.,0.,-1.));
#10274=DIRECTION('',(-1.,0.,0.));
#10275=DIRECTION('center_axis',(1.,0.,0.));
#10276=DIRECTION('ref_axis',(0.,0.,-1.));
#10277=DIRECTION('center_axis',(1.,0.,0.));
#10278=DIRECTION('ref_axis',(0.,0.,-1.));
#12514=CARTESIAN_POINT('',(0.,0.,0.));
#12515=CARTESIAN_POINT('Origin',(12.5,0.,4.));
#12516=CARTESIAN_POINT('',(12.7800042915148,-1.13874042544416E-5,4.45787212683272));
#12517=CARTESIAN_POINT('',(12.6699957084852,1.09516003635735E-5,4.45788309353564));
#12518=CARTESIAN_POINT('',(12.5,-5.60735153159594E-17,4.457875));
#12519=CARTESIAN_POINT('',(12.5,-0.186196943290586,3.58169363627331));
#12520=CARTESIAN_POINT('Ctrl Pts',(12.6699957084852,1.09516003635735E-5,
4.45788309353564));
#12521=CARTESIAN_POINT('Ctrl Pts',(12.6684300766731,0.0150239422001319,
4.45789815019349));
#12522=CARTESIAN_POINT('Ctrl Pts',(12.6668644448611,0.0300354905662504,
4.45717403092565));
#12523=CARTESIAN_POINT('Ctrl Pts',(12.6652988130491,0.0449730203321769,
4.45569984746698));
#12524=CARTESIAN_POINT('Ctrl Pts',(12.6574274409991,0.120072959788606,4.44828824124903));
#12525=CARTESIAN_POINT('Ctrl Pts',(12.6495560689492,0.193301947984492,4.42191743369942));
#12526=CARTESIAN_POINT('Ctrl Pts',(12.6416846968992,0.255884660534875,4.37974732787395));
#12527=CARTESIAN_POINT('Ctrl Pts',(12.6338133248492,0.318467373085258,4.33757722204849));
#12528=CARTESIAN_POINT('Ctrl Pts',(12.6259419527993,0.370403809990138,4.27960781794716));
#12529=CARTESIAN_POINT('Ctrl Pts',(12.6180705807493,0.405471379329245,4.2127856577826));
#12530=CARTESIAN_POINT('Ctrl Pts',(12.6101992086994,0.440538948668352,4.14596349761803));
#12531=CARTESIAN_POINT('Ctrl Pts',(12.6023278366494,0.458737650441686,4.07028858139023));
#12532=CARTESIAN_POINT('Ctrl Pts',(12.5944564645995,0.457884906392306,3.99482861029462));
#12533=CARTESIAN_POINT('Ctrl Pts',(12.5865850925495,0.457032162342926,3.91936863919901));
#12534=CARTESIAN_POINT('Ctrl Pts',(12.5787137204996,0.437127972470831,3.84412361323559));
#12535=CARTESIAN_POINT('Ctrl Pts',(12.5708423484496,0.400561475243013,3.77811083326841));
#12536=CARTESIAN_POINT('Ctrl Pts',(12.5629709763996,0.363994978015195,3.71209805330123));
#12537=CARTESIAN_POINT('Ctrl Pts',(12.5550996043497,0.310766173431653,3.6553175193303));
#12538=CARTESIAN_POINT('Ctrl Pts',(12.5472282322997,0.247245050961511,3.61457214242492));
#12539=CARTESIAN_POINT('Ctrl Pts',(12.5393568602498,0.183723928491369,3.57382676551955));
#12540=CARTESIAN_POINT('Ctrl Pts',(12.5314854881998,0.109910488134627,3.54911654567973));
#12541=CARTESIAN_POINT('Ctrl Pts',(12.5236141161499,0.034670519197381,3.5434092666393));
#12542=CARTESIAN_POINT('Ctrl Pts',(12.5157427440999,-0.0405694497398647,
3.53770198759887));
#12543=CARTESIAN_POINT('Ctrl Pts',(12.50787137205,-0.117235947257613,3.55099764935784));
#12544=CARTESIAN_POINT('Ctrl Pts',(12.5,-0.186196943290592,3.58169363627332));
#12545=CARTESIAN_POINT('',(12.5,-0.186217277007329,4.41832740439831));
#12546=CARTESIAN_POINT('Origin',(12.5,0.,4.));
#12547=CARTESIAN_POINT('Ctrl Pts',(12.5,-0.186217277007329,4.41832740439831));
#12548=CARTESIAN_POINT('Ctrl Pts',(12.5008157411716,-0.193365324225124,
4.41515241707318));
#12549=CARTESIAN_POINT('Ctrl Pts',(12.5016314823431,-0.200430783441492,
4.4117927098014));
#12550=CARTESIAN_POINT('Ctrl Pts',(12.5024472235147,-0.207403505574881,
4.40825058102053));
#12551=CARTESIAN_POINT('Ctrl Pts',(12.5103185955646,-0.274685741688951,
4.37407134077235));
#12552=CARTESIAN_POINT('Ctrl Pts',(12.5181899676146,-0.333333232193243,
4.32290684204764));
#12553=CARTESIAN_POINT('Ctrl Pts',(12.5260613396645,-0.376326743005614,
4.26088786252735));
#12554=CARTESIAN_POINT('Ctrl Pts',(12.5339327117145,-0.419320253817985,
4.19886888300706));
#12555=CARTESIAN_POINT('Ctrl Pts',(12.5418040837645,-0.446659784938435,
4.12599542269119));
#12556=CARTESIAN_POINT('Ctrl Pts',(12.5496754558144,-0.455065168373522,
4.05100019606997));
#12557=CARTESIAN_POINT('Ctrl Pts',(12.5575468278644,-0.463470551808608,
3.97600496944875));
#12558=CARTESIAN_POINT('Ctrl Pts',(12.5654181999143,-0.452941787558331,
3.89888797652218));
#12559=CARTESIAN_POINT('Ctrl Pts',(12.5732895719643,-0.424742400952558,
3.82888990513641));
#12560=CARTESIAN_POINT('Ctrl Pts',(12.5811609440142,-0.396543014346786,
3.75889183375065));
#12561=CARTESIAN_POINT('Ctrl Pts',(12.5890323160642,-0.350673005385519,
3.69601268390568));
#12562=CARTESIAN_POINT('Ctrl Pts',(12.5969036881141,-0.292628022669152,
3.64778723809593));
#12563=CARTESIAN_POINT('Ctrl Pts',(12.6047750601641,-0.234583039952784,
3.59956179228618));
#12564=CARTESIAN_POINT('Ctrl Pts',(12.6126464322141,-0.164363083481316,
3.56599005051166));
#12565=CARTESIAN_POINT('Ctrl Pts',(12.620517804264,-0.0903829156297007,
3.55109483330951));
#12566=CARTESIAN_POINT('Ctrl Pts',(12.628389176314,-0.0164027477780855,
3.53619961610736));
#12567=CARTESIAN_POINT('Ctrl Pts',(12.6362605483639,0.0613376314536766,
3.53998092347757));
#12568=CARTESIAN_POINT('Ctrl Pts',(12.6441319204139,0.13352290298843,3.56198566164487));
#12569=CARTESIAN_POINT('Ctrl Pts',(12.6520032924638,0.205708174523184,3.58399039981218));
#12570=CARTESIAN_POINT('Ctrl Pts',(12.6598746645138,0.272338338360929,3.62421856877658));
#12571=CARTESIAN_POINT('Ctrl Pts',(12.6677460365637,0.325429113408527,3.67784968145944));
#12572=CARTESIAN_POINT('Ctrl Pts',(12.6756174086137,0.378519888456125,3.7314807941423));
#12573=CARTESIAN_POINT('Ctrl Pts',(12.6834887806637,0.418071274713577,3.79851485054363));
#12574=CARTESIAN_POINT('Ctrl Pts',(12.6913601527136,0.439343931585728,3.87091926467948));
#12575=CARTESIAN_POINT('Ctrl Pts',(12.6992315247636,0.460616588457879,3.94332367881533));
#12576=CARTESIAN_POINT('Ctrl Pts',(12.7071028968135,0.46361051594473,4.02109845068571));
#12577=CARTESIAN_POINT('Ctrl Pts',(12.7149742688635,0.447966936692366,4.09492394607626));
#12578=CARTESIAN_POINT('Ctrl Pts',(12.7228456409134,0.432323357440003,4.16874944146681));
#12579=CARTESIAN_POINT('Ctrl Pts',(12.7307170129634,0.398042271448426,4.23862566037754));
#12580=CARTESIAN_POINT('Ctrl Pts',(12.7385883850133,0.349231538304918,4.29617944234672));
#12581=CARTESIAN_POINT('Ctrl Pts',(12.7464597570633,0.300420805161409,4.35373322431589));
#12582=CARTESIAN_POINT('Ctrl Pts',(12.7543311291133,0.237080424865968,4.39896456934351));
#12583=CARTESIAN_POINT('Ctrl Pts',(12.7622025011632,0.166800374688878,4.42645347375649));
#12584=CARTESIAN_POINT('Ctrl Pts',(12.7681364312804,0.113818899065861,4.4471763206439));
#12585=CARTESIAN_POINT('Ctrl Pts',(12.7740703613976,0.056893551674301,4.45781599184163));
#12586=CARTESIAN_POINT('Ctrl Pts',(12.7800042915148,-1.13874042544416E-5,
4.45787212683272));
#12587=CARTESIAN_POINT('Origin',(12.5,0.,4.));
#12588=CARTESIAN_POINT('',(13.0800042915148,2.8196954984682E-6,4.45783894202495));
#12589=CARTESIAN_POINT('',(12.9699957084852,-6.90274666573233E-6,4.45790451736119));
#12590=CARTESIAN_POINT('',(12.5,-5.60735153159594E-17,4.457875));
#12591=CARTESIAN_POINT('Ctrl Pts',(12.9699957084852,-6.90274666573233E-6,
4.45790451736119));
#12592=CARTESIAN_POINT('Ctrl Pts',(12.9628865412726,0.0681543496286777,
4.45785453236543));
#12593=CARTESIAN_POINT('Ctrl Pts',(12.95577737406,0.136337475731944,4.44242789501186));
#12594=CARTESIAN_POINT('Ctrl Pts',(12.9486682068475,0.197807532932104,4.41298560914613));
#12595=CARTESIAN_POINT('Ctrl Pts',(12.9407968347975,0.265868063186489,4.38038668734267));
#12596=CARTESIAN_POINT('Ctrl Pts',(12.9329254627476,0.325698883531032,4.33060565060516));
#12597=CARTESIAN_POINT('Ctrl Pts',(12.9250540906976,0.370130557623211,4.26960768492436));
#12598=CARTESIAN_POINT('Ctrl Pts',(12.9171827186476,0.41456223171539,4.20860971924356));
#12599=CARTESIAN_POINT('Ctrl Pts',(12.9093113465977,0.443594759555206,4.13639482461947));
#12600=CARTESIAN_POINT('Ctrl Pts',(12.9014399745477,0.453749217534713,4.06161640217293));
#12601=CARTESIAN_POINT('Ctrl Pts',(12.8935686024978,0.463903675514219,3.9868379797264));
#12602=CARTESIAN_POINT('Ctrl Pts',(12.8856972304478,0.455180063633418,3.90949602945742));
#12603=CARTESIAN_POINT('Ctrl Pts',(12.8778258583979,0.428623718850503,3.83885831972366));
#12604=CARTESIAN_POINT('Ctrl Pts',(12.8699544863479,0.402067374067587,3.7682206099899));
#12605=CARTESIAN_POINT('Ctrl Pts',(12.862083114298,0.357678296382559,3.70428714079136));
#12606=CARTESIAN_POINT('Ctrl Pts',(12.854211742248,0.300775561959983,3.65471896268111));
#12607=CARTESIAN_POINT('Ctrl Pts',(12.846340370198,0.243872827537407,3.60515078457087));
#12608=CARTESIAN_POINT('Ctrl Pts',(12.8384689981481,0.174456436377283,3.56994789754891));
#12609=CARTESIAN_POINT('Ctrl Pts',(12.8305976260981,0.100844448250471,3.55332860992135));
#12610=CARTESIAN_POINT('Ctrl Pts',(12.8227262540482,0.0272324601236582,
3.53670932229378));
#12611=CARTESIAN_POINT('Ctrl Pts',(12.8148548819982,-0.0505751249698428,
3.53867363406062));
#12612=CARTESIAN_POINT('Ctrl Pts',(12.8069835099483,-0.123254740362562,
3.558986165072));
#12613=CARTESIAN_POINT('Ctrl Pts',(12.7991121378983,-0.195934355755281,
3.57929869608338));
#12614=CARTESIAN_POINT('Ctrl Pts',(12.7912407658484,-0.263486001447217,
3.6179594463393));
#12615=CARTESIAN_POINT('Ctrl Pts',(12.7833693937984,-0.317815070570116,
3.67033575613656));
#12616=CARTESIAN_POINT('Ctrl Pts',(12.7754980217484,-0.372144139693014,
3.72271206593382));
#12617=CARTESIAN_POINT('Ctrl Pts',(12.7676266496985,-0.413250632246875,
3.78880393527241));
#12618=CARTESIAN_POINT('Ctrl Pts',(12.7597552776485,-0.43620881068128,3.86069167744737));
#12619=CARTESIAN_POINT('Ctrl Pts',(12.7518839055986,-0.459166989115684,
3.93257941962233));
#12620=CARTESIAN_POINT('Ctrl Pts',(12.7440125335486,-0.463976853430633,
4.01026303463365));
#12621=CARTESIAN_POINT('Ctrl Pts',(12.7361411614987,-0.450062064178823,
4.08443380953254));
#12622=CARTESIAN_POINT('Ctrl Pts',(12.7282697894487,-0.436147274927012,
4.15860458443143));
#12623=CARTESIAN_POINT('Ctrl Pts',(12.7203984173988,-0.403507832108441,
4.22926251921788));
#12624=CARTESIAN_POINT('Ctrl Pts',(12.7125270453488,-0.356054829243877,
4.28794078818664));
#12625=CARTESIAN_POINT('Ctrl Pts',(12.7046556732988,-0.308601826379312,
4.3466190571554));
#12626=CARTESIAN_POINT('Ctrl Pts',(12.6967843012489,-0.246335263468753,
4.39331766030646));
#12627=CARTESIAN_POINT('Ctrl Pts',(12.6889129291989,-0.176716536654988,
4.42244075943884));
#12628=CARTESIAN_POINT('Ctrl Pts',(12.682607188961,-0.120945115332726,4.44577121528397));
#12629=CARTESIAN_POINT('Ctrl Pts',(12.6763014487231,-0.0604553842193124,
4.45782245132557));
#12630=CARTESIAN_POINT('Ctrl Pts',(12.6699957084852,1.09516003635735E-5,
4.45788309353564));
#12631=CARTESIAN_POINT('Ctrl Pts',(12.7800042915148,-1.13874042544416E-5,
4.45787212683272));
#12632=CARTESIAN_POINT('Ctrl Pts',(12.7819417334476,-0.0185909818676029,
4.45789045503738));
#12633=CARTESIAN_POINT('Ctrl Pts',(12.7838791753803,-0.0371684007279871,
4.45678053845584));
#12634=CARTESIAN_POINT('Ctrl Pts',(12.7858166173131,-0.0556056617636943,
4.45452496135198));
#12635=CARTESIAN_POINT('Ctrl Pts',(12.793687989363,-0.130511927980435,4.44536108073615));
#12636=CARTESIAN_POINT('Ctrl Pts',(12.801559361413,-0.203104740355178,4.41728685570614));
#12637=CARTESIAN_POINT('Ctrl Pts',(12.8094307334629,-0.264685413403174,
4.37366637792357));
#12638=CARTESIAN_POINT('Ctrl Pts',(12.8173021055129,-0.32626608645117,4.33004590014099));
#12639=CARTESIAN_POINT('Ctrl Pts',(12.8251734775629,-0.37683462017242,4.27087916960585));
#12640=CARTESIAN_POINT('Ctrl Pts',(12.8330448496128,-0.410331463567461,
4.20325604577686));
#12641=CARTESIAN_POINT('Ctrl Pts',(12.8409162216628,-0.443828306962503,
4.13563292194788));
#12642=CARTESIAN_POINT('Ctrl Pts',(12.8487875937127,-0.460253460031337,
4.05955340482505));
#12643=CARTESIAN_POINT('Ctrl Pts',(12.8566589657627,-0.457638721839564,
3.98413398734005));
#12644=CARTESIAN_POINT('Ctrl Pts',(12.8645303378126,-0.45502398364779,3.90871456985506));
#12645=CARTESIAN_POINT('Ctrl Pts',(12.8724017098626,-0.433369354195409,
3.8339552520079));
#12646=CARTESIAN_POINT('Ctrl Pts',(12.8802730819125,-0.395269674734573,
3.76881432927916));
#12647=CARTESIAN_POINT('Ctrl Pts',(12.8881444539625,-0.357169995273737,
3.70367340655041));
#12648=CARTESIAN_POINT('Ctrl Pts',(12.8960158260125,-0.302625265804445,
3.64815087894007));
#12649=CARTESIAN_POINT('Ctrl Pts',(12.9038871980624,-0.238171498431664,
3.6088999265713));
#12650=CARTESIAN_POINT('Ctrl Pts',(12.9117585701124,-0.173717731058884,
3.56964897420252));
#12651=CARTESIAN_POINT('Ctrl Pts',(12.9196299421623,-0.0993549257826154,
3.5466695970753));
#12652=CARTESIAN_POINT('Ctrl Pts',(12.9275013142123,-0.023993864556795,
3.54271537903906));
#12653=CARTESIAN_POINT('Ctrl Pts',(12.9353726862622,0.0513671966690251,
3.53876116100282));
#12654=CARTESIAN_POINT('Ctrl Pts',(12.9432440583122,0.127726513844396,3.55383210205756));
#12655=CARTESIAN_POINT('Ctrl Pts',(12.9511154303621,0.195934065997641,3.58612227423372));
#12656=CARTESIAN_POINT('Ctrl Pts',(12.9589868024121,0.264141618150887,3.61841244640988));
#12657=CARTESIAN_POINT('Ctrl Pts',(12.9668581744621,0.324197405282005,3.66792184970745));
#12658=CARTESIAN_POINT('Ctrl Pts',(12.974729546512,0.368905033668178,3.72871784755079));
#12659=CARTESIAN_POINT('Ctrl Pts',(12.982600918562,0.41361266205435,3.78951384539413));
#12660=CARTESIAN_POINT('Ctrl Pts',(12.9904722906119,0.442972131695578,3.86159643778324));
#12661=CARTESIAN_POINT('Ctrl Pts',(12.9983436626619,0.453465341949404,3.93632807718928));
#12662=CARTESIAN_POINT('Ctrl Pts',(13.0062150347118,0.46395855220323,4.01105971659532));
#12663=CARTESIAN_POINT('Ctrl Pts',(13.0140864067618,0.455585503069655,4.0884404030183));
#12664=CARTESIAN_POINT('Ctrl Pts',(13.0219577788117,0.429349524305901,4.15919772637108));
#12665=CARTESIAN_POINT('Ctrl Pts',(13.0298291508617,0.403113545542148,4.22995504972387));
#12666=CARTESIAN_POINT('Ctrl Pts',(13.0377005229117,0.359014637148215,4.29408901000646));
#12667=CARTESIAN_POINT('Ctrl Pts',(13.0455718949616,0.302337104315659,4.34391453219887));
#12668=CARTESIAN_POINT('Ctrl Pts',(13.0534432670116,0.245659571483104,4.39374005439127));
#12669=CARTESIAN_POINT('Ctrl Pts',(13.0613146390615,0.176403414211925,4.4292571384935));
#12670=CARTESIAN_POINT('Ctrl Pts',(13.0691860111115,0.102867492605122,4.44620982627979));
#12671=CARTESIAN_POINT('Ctrl Pts',(13.0727921045793,0.0691786509558273,
4.45397632191734));
#12672=CARTESIAN_POINT('Ctrl Pts',(13.076398198047,0.0345915681853763,4.45784650391406));
#12673=CARTESIAN_POINT('Ctrl Pts',(13.0800042915148,2.8196954984682E-6,
4.45783894202495));
#12674=CARTESIAN_POINT('Origin',(12.5,0.,4.));
#12675=CARTESIAN_POINT('',(13.3800042915148,1.00338821889499E-5,4.45789143379912));
#12676=CARTESIAN_POINT('',(13.2699957084852,-6.83105689078257E-6,4.45784477598907));
#12677=CARTESIAN_POINT('',(12.5,-5.60735153159594E-17,4.457875));
#12678=CARTESIAN_POINT('Ctrl Pts',(13.2699957084852,-6.83105689078257E-6,
4.45784477598907));
#12679=CARTESIAN_POINT('Ctrl Pts',(13.265214377922,0.0458528260712244,4.45782008288951));
#12680=CARTESIAN_POINT('Ctrl Pts',(13.2604330473589,0.091719698604501,4.45096974854549));
#12681=CARTESIAN_POINT('Ctrl Pts',(13.2556517167957,0.135506404234727,4.43740478719402));
#12682=CARTESIAN_POINT('Ctrl Pts',(13.2477803447458,0.207591244700251,4.41507316710824));
#12683=CARTESIAN_POINT('Ctrl Pts',(13.2399089726958,0.274038390871736,4.37454348113122));
#12684=CARTESIAN_POINT('Ctrl Pts',(13.2320376006459,0.326885582178656,4.32067233995558));
#12685=CARTESIAN_POINT('Ctrl Pts',(13.2241662285959,0.379732773485576,4.26680119877995));
#12686=CARTESIAN_POINT('Ctrl Pts',(13.2162948565459,0.418980009927931,4.19958860240569));
#12687=CARTESIAN_POINT('Ctrl Pts',(13.208423484496,0.439924354792367,4.12708853413817));
#12688=CARTESIAN_POINT('Ctrl Pts',(13.200552112446,0.460868699656804,4.05458846587065));
#12689=CARTESIAN_POINT('Ctrl Pts',(13.1926807403961,0.463510152943321,3.97680092570987));
#12690=CARTESIAN_POINT('Ctrl Pts',(13.1848093683461,0.447532193317848,3.90304707640827));
#12691=CARTESIAN_POINT('Ctrl Pts',(13.1769379962962,0.431554233692375,3.82929322710668));
#12692=CARTESIAN_POINT('Ctrl Pts',(13.1690666242462,0.396956861154912,3.75957306866428));
#12693=CARTESIAN_POINT('Ctrl Pts',(13.1611952521963,0.347885826291745,3.70224106173923));
#12694=CARTESIAN_POINT('Ctrl Pts',(13.1533238801463,0.298814791428577,3.64490905481418));
#12695=CARTESIAN_POINT('Ctrl Pts',(13.1454525080963,0.235270094239705,3.59996519940648));
#12696=CARTESIAN_POINT('Ctrl Pts',(13.1375811360464,0.164866199243897,3.57279504942506));
#12697=CARTESIAN_POINT('Ctrl Pts',(13.1297097639964,0.0944623042480882,
3.54562489944363));
#12698=CARTESIAN_POINT('Ctrl Pts',(13.1218383919465,0.0171992114453437,
3.53622845488849));
#12699=CARTESIAN_POINT('Ctrl Pts',(13.1139670198965,-0.0576647601420857,
3.54573167743434));
#12700=CARTESIAN_POINT('Ctrl Pts',(13.1060956478466,-0.132528731729515,
3.55523489998019));
#12701=CARTESIAN_POINT('Ctrl Pts',(13.0982242757966,-0.204993582101629,
3.58363778962703));
#12702=CARTESIAN_POINT('Ctrl Pts',(13.0903529037467,-0.266375958336211,
3.62753687126191));
#12703=CARTESIAN_POINT('Ctrl Pts',(13.0824815316967,-0.327758334570793,
3.67143595289679));
#12704=CARTESIAN_POINT('Ctrl Pts',(13.0746101596467,-0.378058236667844,
3.73083122651971));
#12705=CARTESIAN_POINT('Ctrl Pts',(13.0667387875968,-0.411248303781717,
3.79860544673343));
#12706=CARTESIAN_POINT('Ctrl Pts',(13.0588674155468,-0.444438370895591,
3.86637966694714));
#12707=CARTESIAN_POINT('Ctrl Pts',(13.0509960434969,-0.460518603026287,
3.94253283375165));
#12708=CARTESIAN_POINT('Ctrl Pts',(13.0431246714469,-0.457562130387816,
4.0179396288708));
#12709=CARTESIAN_POINT('Ctrl Pts',(13.035253299397,-0.454605657749345,4.09334642398995));
#12710=CARTESIAN_POINT('Ctrl Pts',(13.027381927347,-0.432612480341706,4.16800684742375));
#12711=CARTESIAN_POINT('Ctrl Pts',(13.0195105552971,-0.394218007200806,
4.23297445406563));
#12712=CARTESIAN_POINT('Ctrl Pts',(13.0116391832471,-0.355823534059905,
4.29794206070751));
#12713=CARTESIAN_POINT('Ctrl Pts',(13.0037678111972,-0.301027765185743,
4.35321685055749));
#12714=CARTESIAN_POINT('Ctrl Pts',(12.9958964391472,-0.236396794305188,
4.39217532952931));
#12715=CARTESIAN_POINT('Ctrl Pts',(12.9880250670972,-0.171765823424632,
4.43113380850113));
#12716=CARTESIAN_POINT('Ctrl Pts',(12.9801536950473,-0.0972996505376846,
4.45377597659478));
#12717=CARTESIAN_POINT('Ctrl Pts',(12.9722823229973,-0.0219214440120968,
4.4573886572069));
#12718=CARTESIAN_POINT('Ctrl Pts',(12.9715201181599,-0.014622381881285,
4.45773848219561));
#12719=CARTESIAN_POINT('Ctrl Pts',(12.9707579133226,-0.00731476803234869,
4.45790987647069));
#12720=CARTESIAN_POINT('Ctrl Pts',(12.9699957084852,-6.90274666573233E-6,
4.45790451736119));
#12721=CARTESIAN_POINT('Ctrl Pts',(13.0800042915148,2.8196954984682E-6,
4.45783894202495));
#12722=CARTESIAN_POINT('Ctrl Pts',(13.084269570097,-0.0409086678841046,
4.4578299978409));
#12723=CARTESIAN_POINT('Ctrl Pts',(13.0885348486792,-0.0818224858219862,
4.45239605085009));
#12724=CARTESIAN_POINT('Ctrl Pts',(13.0928001272613,-0.121255029803553,
4.44156782927524));
#12725=CARTESIAN_POINT('Ctrl Pts',(13.1006714993113,-0.194025944662995,
4.42158485301405));
#12726=CARTESIAN_POINT('Ctrl Pts',(13.1085428713613,-0.261752088439453,
4.3832306090213));
#12727=CARTESIAN_POINT('Ctrl Pts',(13.1164142434112,-0.31631794022257,4.33110102808186));
#12728=CARTESIAN_POINT('Ctrl Pts',(13.1242856154612,-0.370883792005687,
4.27897144714243));
#12729=CARTESIAN_POINT('Ctrl Pts',(13.1321569875111,-0.412289351795463,
4.21306652925631));
#12730=CARTESIAN_POINT('Ctrl Pts',(13.1400283595611,-0.435573054271055,
4.14128356060242));
#12731=CARTESIAN_POINT('Ctrl Pts',(13.147899731611,-0.458856756746647,4.06950059194853));
#12732=CARTESIAN_POINT('Ctrl Pts',(13.155771103661,-0.464018601908056,3.99183957252686));
#12733=CARTESIAN_POINT('Ctrl Pts',(13.1636424757109,-0.45044005369213,3.91760650430194));
#12734=CARTESIAN_POINT('Ctrl Pts',(13.1715138477609,-0.436861505476204,
3.84337343607703));
#12735=CARTESIAN_POINT('Ctrl Pts',(13.1793852198109,-0.404542563882944,
3.77256831904885));
#12736=CARTESIAN_POINT('Ctrl Pts',(13.1872565918608,-0.357355958580309,
3.7136756228145));
#12737=CARTESIAN_POINT('Ctrl Pts',(13.1951279639108,-0.310169353277673,
3.65478292658016));
#12738=CARTESIAN_POINT('Ctrl Pts',(13.2029993359607,-0.248115084265664,
3.60780265113964));
#12739=CARTESIAN_POINT('Ctrl Pts',(13.2108707080107,-0.178629020319019,
3.57836437152041));
#12740=CARTESIAN_POINT('Ctrl Pts',(13.2187420800606,-0.109142956372374,
3.54892609190117));
#12741=CARTESIAN_POINT('Ctrl Pts',(13.2266134521106,-0.0322250974910928,
3.53702980810322));
#12742=CARTESIAN_POINT('Ctrl Pts',(13.2344848241605,0.0429076061587562,
3.54410103373967));
#12743=CARTESIAN_POINT('Ctrl Pts',(13.2423561962105,0.118040309808605,3.55117225937612));
#12744=CARTESIAN_POINT('Ctrl Pts',(13.2502275682605,0.191387858227023,3.57721099444696));
#12745=CARTESIAN_POINT('Ctrl Pts',(13.2580989403104,0.254161126126225,3.61909705689013));
#12746=CARTESIAN_POINT('Ctrl Pts',(13.2659703123604,0.316934394025428,3.66098311933329));
#12747=CARTESIAN_POINT('Ctrl Pts',(13.2738416844103,0.369133381405416,3.71871650914877));
#12748=CARTESIAN_POINT('Ctrl Pts',(13.2817130564603,0.404503162915977,3.78537912195109));
#12749=CARTESIAN_POINT('Ctrl Pts',(13.2895844285102,0.43987294442654,3.85204173475342));
#12750=CARTESIAN_POINT('Ctrl Pts',(13.2974558005602,0.458413520067676,3.92763357054259));
#12751=CARTESIAN_POINT('Ctrl Pts',(13.3053271726101,0.457903200829578,4.00309657448501));
#12752=CARTESIAN_POINT('Ctrl Pts',(13.3131985446601,0.457392881591479,4.07855957842742));
#12753=CARTESIAN_POINT('Ctrl Pts',(13.3210699167101,0.437831667474148,4.15389375052308));
#12754=CARTESIAN_POINT('Ctrl Pts',(13.32894128876,0.401563549045306,4.22007191138728));
#12755=CARTESIAN_POINT('Ctrl Pts',(13.33681266081,0.365295430616463,4.28625007225149));
#12756=CARTESIAN_POINT('Ctrl Pts',(13.3446840328599,0.31232040787611,4.34327222188425));
#12757=CARTESIAN_POINT('Ctrl Pts',(13.3525554049099,0.248986397312635,4.38430548273058));
#12758=CARTESIAN_POINT('Ctrl Pts',(13.3604267769598,0.185652386749161,4.42533874357692));
#12759=CARTESIAN_POINT('Ctrl Pts',(13.3682981490098,0.111959388362564,4.45038311563682));
#12760=CARTESIAN_POINT('Ctrl Pts',(13.3761695210597,0.0367379221854645,
4.45643756985705));
#12761=CARTESIAN_POINT('Ctrl Pts',(13.3774477778781,0.024522472144774,4.45742077168506));
#12762=CARTESIAN_POINT('Ctrl Pts',(13.3787260346965,0.0122667140672706,
4.45790318029249));
#12763=CARTESIAN_POINT('Ctrl Pts',(13.3800042915148,1.00338821889499E-5,
4.45789143379912));
#12764=CARTESIAN_POINT('Origin',(12.5,0.,4.));
#12765=CARTESIAN_POINT('',(13.6800042915148,-8.85210990424201E-6,4.45789764648838));
#12766=CARTESIAN_POINT('',(13.5699957084852,1.03170790782398E-5,4.4578580083501));
#12767=CARTESIAN_POINT('',(12.5,-5.60735153159594E-17,4.457875));
#12768=CARTESIAN_POINT('Ctrl Pts',(13.5699957084852,1.03170790782398E-5,
4.4578580083501));
#12769=CARTESIAN_POINT('Ctrl Pts',(13.5675422145714,0.0235408097699949,
4.45787795556699));
#12770=CARTESIAN_POINT('Ctrl Pts',(13.5650887206577,0.0470683081483061,
4.45609516914004));
#12771=CARTESIAN_POINT('Ctrl Pts',(13.562635226744,0.0703115975725277,4.45248338388903));
#12772=CARTESIAN_POINT('Ctrl Pts',(13.554763854694,0.144881409096958,4.44089594716616));
#12773=CARTESIAN_POINT('Ctrl Pts',(13.5468924826441,0.21652593236894,4.41048310506186));
#12774=CARTESIAN_POINT('Ctrl Pts',(13.5390211105941,0.276660113016528,4.36488918223832));
#12775=CARTESIAN_POINT('Ctrl Pts',(13.5311497385442,0.336794293664116,4.31929525941478));
#12776=CARTESIAN_POINT('Ctrl Pts',(13.5232783664942,0.385418131687311,4.25852025587201));
#12777=CARTESIAN_POINT('Ctrl Pts',(13.5154069944443,0.416705106451492,4.18984674794718));
#12778=CARTESIAN_POINT('Ctrl Pts',(13.5075356223943,0.447992081215673,4.12117324002235));
#12779=CARTESIAN_POINT('Ctrl Pts',(13.4996642503443,0.461942192720839,4.04460122771548));
#12780=CARTESIAN_POINT('Ctrl Pts',(13.4917928782944,0.456883820300162,3.96930621892307));
#12781=CARTESIAN_POINT('Ctrl Pts',(13.4839215062444,0.451825447879485,3.89401121013066));
#12782=CARTESIAN_POINT('Ctrl Pts',(13.4760501341945,0.427758591532965,3.81999320485271));
#12783=CARTESIAN_POINT('Ctrl Pts',(13.4681787621445,0.387567146091087,3.75612166820384));
#12784=CARTESIAN_POINT('Ctrl Pts',(13.4603073900946,0.347375700649209,3.69225013155497));
#12785=CARTESIAN_POINT('Ctrl Pts',(13.4524360180446,0.291059666111973,3.63852506353517));
#12786=CARTESIAN_POINT('Ctrl Pts',(13.4445646459947,0.225367307335285,3.60138425741911));
#12787=CARTESIAN_POINT('Ctrl Pts',(13.4366932739447,0.159674948558598,3.56424345130305));
#12788=CARTESIAN_POINT('Ctrl Pts',(13.4288219018947,0.0846062655424597,
3.54368690709073));
#12789=CARTESIAN_POINT('Ctrl Pts',(13.4209505298448,0.00915662451852634,
3.54217788424291));
#12790=CARTESIAN_POINT('Ctrl Pts',(13.4130791577948,-0.0662930165054059,
3.54066886139509));
#12791=CARTESIAN_POINT('Ctrl Pts',(13.4052077857449,-0.142123615537132,
3.55820735991178));
#12792=CARTESIAN_POINT('Ctrl Pts',(13.3973364136949,-0.209248507106454,
3.5926917681625));
#12793=CARTESIAN_POINT('Ctrl Pts',(13.389465041645,-0.276373398675776,3.62717617641322));
#12794=CARTESIAN_POINT('Ctrl Pts',(13.381593669595,-0.334792582782693,3.67860649439798));
#12795=CARTESIAN_POINT('Ctrl Pts',(13.3737222975451,-0.377505777353741,
3.74081990525232));
#12796=CARTESIAN_POINT('Ctrl Pts',(13.3658509254951,-0.420218971924789,
3.80303331610666));
#12797=CARTESIAN_POINT('Ctrl Pts',(13.3579795534451,-0.44722617695997,3.87602981983059));
#12798=CARTESIAN_POINT('Ctrl Pts',(13.3501081813952,-0.455291160112798,
3.95106235628872));
#12799=CARTESIAN_POINT('Ctrl Pts',(13.3422368093452,-0.463356143265626,
4.02609489274685));
#12800=CARTESIAN_POINT('Ctrl Pts',(13.3343654372953,-0.452478904536101,
4.10316346193917));
#12801=CARTESIAN_POINT('Ctrl Pts',(13.3264940652453,-0.423962846915058,
4.17303305431203));
#12802=CARTESIAN_POINT('Ctrl Pts',(13.3186226931954,-0.395446789294015,
4.24290264668488));
#12803=CARTESIAN_POINT('Ctrl Pts',(13.3107513211454,-0.349291912781453,
4.30557326223827));
#12804=CARTESIAN_POINT('Ctrl Pts',(13.3028799490955,-0.291028886105345,
4.35353517632783));
#12805=CARTESIAN_POINT('Ctrl Pts',(13.2950085770455,-0.232765859429236,
4.4014970904174));
#12806=CARTESIAN_POINT('Ctrl Pts',(13.2871372049956,-0.162394682589579,
4.43475030304313));
#12807=CARTESIAN_POINT('Ctrl Pts',(13.2792658329456,-0.0883478267899694,
4.44931013225873));
#12808=CARTESIAN_POINT('Ctrl Pts',(13.2761757914588,-0.059279469337623,
4.4550258417985));
#12809=CARTESIAN_POINT('Ctrl Pts',(13.273085749972,-0.0296446570187532,
4.45786073445524));
#12810=CARTESIAN_POINT('Ctrl Pts',(13.2699957084852,-6.83105689078257E-6,
4.45784477598907));
#12811=CARTESIAN_POINT('Ctrl Pts',(13.3800042915148,1.00338821889499E-5,
4.45789143379912));
#12812=CARTESIAN_POINT('Ctrl Pts',(13.3865974067464,-0.0632086430349686,
4.45783084661254));
#12813=CARTESIAN_POINT('Ctrl Pts',(13.393190521978,-0.12645185159805,4.44462381290384));
#12814=CARTESIAN_POINT('Ctrl Pts',(13.3997836372096,-0.184315051738561,
4.41918121595096));
#12815=CARTESIAN_POINT('Ctrl Pts',(13.4076550092596,-0.253396625517876,
4.3888058714441));
#12816=CARTESIAN_POINT('Ctrl Pts',(13.4155263813095,-0.314809839108902,
4.34099064604983));
#12817=CARTESIAN_POINT('Ctrl Pts',(13.4233977533595,-0.361195640434018,
4.28146516557999));
#12818=CARTESIAN_POINT('Ctrl Pts',(13.4312691254094,-0.407581441759134,
4.22193968511016));
#12819=CARTESIAN_POINT('Ctrl Pts',(13.4391404974594,-0.438939830818339,
4.15070394956476));
#12820=CARTESIAN_POINT('Ctrl Pts',(13.4470118695093,-0.451513179494438,
4.07629402890356));
#12821=CARTESIAN_POINT('Ctrl Pts',(13.4548832415593,-0.464086528170537,
4.00188410824235));
#12822=CARTESIAN_POINT('Ctrl Pts',(13.4627546136093,-0.457874836463529,
3.92430000246534));
#12823=CARTESIAN_POINT('Ctrl Pts',(13.4706259856592,-0.433622441953051,
3.85283849709185));
#12824=CARTESIAN_POINT('Ctrl Pts',(13.4784973577092,-0.409370047442573,
3.78137699171835));
#12825=CARTESIAN_POINT('Ctrl Pts',(13.4863687297591,-0.367076950128625,
3.71603808674838));
#12826=CARTESIAN_POINT('Ctrl Pts',(13.4942401018091,-0.311811067605128,
3.66465124389307));
#12827=CARTESIAN_POINT('Ctrl Pts',(13.502111473859,-0.25654518508163,3.61326440103776));
#12828=CARTESIAN_POINT('Ctrl Pts',(13.509982845909,-0.188306517348584,3.5758296202971));
#12829=CARTESIAN_POINT('Ctrl Pts',(13.5178542179589,-0.115272000283325,
3.55683265457144));
#12830=CARTESIAN_POINT('Ctrl Pts',(13.5257255900089,-0.0422374832180674,
3.53783568884578));
#12831=CARTESIAN_POINT('Ctrl Pts',(13.5335969620589,0.035592883179403,3.53727653813511));
#12832=CARTESIAN_POINT('Ctrl Pts',(13.5414683341088,0.108892804353757,3.55522220461956));
#12833=CARTESIAN_POINT('Ctrl Pts',(13.5493397061588,0.182192725528112,3.573167871104));
#12834=CARTESIAN_POINT('Ctrl Pts',(13.5572110782087,0.250962201479351,3.60961835478357));
#12835=CARTESIAN_POINT('Ctrl Pts',(13.5650824502587,0.306960690387823,3.66020584957927));
#12836=CARTESIAN_POINT('Ctrl Pts',(13.5729538223086,0.362959179296295,3.71079334437498));
#12837=CARTESIAN_POINT('Ctrl Pts',(13.5808251943586,0.406186681162,3.77551785028682));
#12838=CARTESIAN_POINT('Ctrl Pts',(13.5886965664085,0.431463310113251,3.84662352810933));
#12839=CARTESIAN_POINT('Ctrl Pts',(13.5965679384585,0.456739939064502,3.91772920593184));
#12840=CARTESIAN_POINT('Ctrl Pts',(13.6044393105085,0.464065695101298,3.99521605566501));
#12841=CARTESIAN_POINT('Ctrl Pts',(13.6123106825584,0.452562744007997,4.06979894583348));
#12842=CARTESIAN_POINT('Ctrl Pts',(13.6201820546084,0.441059792914696,4.14438183600196));
#12843=CARTESIAN_POINT('Ctrl Pts',(13.6280534266583,0.410728134691299,4.21606076660573));
#12844=CARTESIAN_POINT('Ctrl Pts',(13.6359247987083,0.365202365858889,4.27624656029457));
#12845=CARTESIAN_POINT('Ctrl Pts',(13.6437961707582,0.319676597026479,4.33643235398341));
#12846=CARTESIAN_POINT('Ctrl Pts',(13.6516675428082,0.258956717585058,4.38512501075732));
#12847=CARTESIAN_POINT('Ctrl Pts',(13.6595389148581,0.190318698434502,4.41648976353532));
#12848=CARTESIAN_POINT('Ctrl Pts',(13.666360707077,0.130832969391341,4.44367229602021));
#12849=CARTESIAN_POINT('Ctrl Pts',(13.6731824992959,0.065399948454096,4.45783988979956));
#12850=CARTESIAN_POINT('Ctrl Pts',(13.6800042915148,-8.85210990424201E-6,
4.45789764648838));
#12851=CARTESIAN_POINT('Origin',(12.5,0.,4.));
#12852=CARTESIAN_POINT('',(13.9800042915148,-4.68615130337092E-6,4.45784092071359));
#12853=CARTESIAN_POINT('',(13.8699957084852,1.23414887176878E-6,4.4579133809027));
#12854=CARTESIAN_POINT('',(12.5,-5.60735153159594E-17,4.457875));
#12855=CARTESIAN_POINT('Ctrl Pts',(13.8699957084852,1.23414887176878E-6,
4.4579133809027));
#12856=CARTESIAN_POINT('Ctrl Pts',(13.8698700512209,0.00120594270822336,
4.45791357044259));
#12857=CARTESIAN_POINT('Ctrl Pts',(13.8697443939566,0.00241064979645091,
4.45790891401425));
#12858=CARTESIAN_POINT('Ctrl Pts',(13.8696187366923,0.00361531855258033,
4.45789940262096));
#12859=CARTESIAN_POINT('Ctrl Pts',(13.8617473646423,0.0790776965455978,
4.45730359373015));
#12860=CARTESIAN_POINT('Ctrl Pts',(13.8538759925924,0.154389660535011,4.43765704798318));
#12861=CARTESIAN_POINT('Ctrl Pts',(13.8460046205424,0.22052669229976,4.40131398110731));
#12862=CARTESIAN_POINT('Ctrl Pts',(13.8381332484924,0.286663724064511,4.36497091423144));
#12863=CARTESIAN_POINT('Ctrl Pts',(13.8302618764425,0.343625823604597,4.31193132622667));
#12864=CARTESIAN_POINT('Ctrl Pts',(13.8223905043925,0.384587309076409,4.24855087033892));
#12865=CARTESIAN_POINT('Ctrl Pts',(13.8145191323426,0.42554879454822,4.18517041445118));
#12866=CARTESIAN_POINT('Ctrl Pts',(13.8066477602926,0.450509665951756,4.11144909068046));
#12867=CARTESIAN_POINT('Ctrl Pts',(13.7987763882427,0.456478899990553,4.03622081324714));
#12868=CARTESIAN_POINT('Ctrl Pts',(13.7909050161927,0.46244813402935,3.96099253581381));
#12869=CARTESIAN_POINT('Ctrl Pts',(13.7830336441427,0.449425730703409,3.88425730471787));
#12870=CARTESIAN_POINT('Ctrl Pts',(13.7751622720928,0.418972144817937,3.81521018611534));
#12871=CARTESIAN_POINT('Ctrl Pts',(13.7672909000428,0.388518558932466,3.74616306751281));
#12872=CARTESIAN_POINT('Ctrl Pts',(13.7594195279929,0.340633790487464,3.68480406140369));
#12873=CARTESIAN_POINT('Ctrl Pts',(13.7515481559429,0.281055798532888,3.6384857242654));
#12874=CARTESIAN_POINT('Ctrl Pts',(13.743676783893,0.221477806578313,3.59216738712712));
#12875=CARTESIAN_POINT('Ctrl Pts',(13.735805411843,0.150206591114165,3.56088971895966));
#12876=CARTESIAN_POINT('Ctrl Pts',(13.7279340397931,0.0757824736049535,
3.54840067521841));
#12877=CARTESIAN_POINT('Ctrl Pts',(13.7200626677431,0.00135835609574232,
3.53591163147717));
#12878=CARTESIAN_POINT('Ctrl Pts',(13.7121912956931,-0.0762186634585312,
3.54221121216214));
#12879=CARTESIAN_POINT('Ctrl Pts',(13.7043199236432,-0.14765264866984,3.56654454809098));
#12880=CARTESIAN_POINT('Ctrl Pts',(13.6964485515932,-0.219086633881149,
3.59087788401983));
#12881=CARTESIAN_POINT('Ctrl Pts',(13.6885771795433,-0.284377584749494,
3.63324497519255));
#12882=CARTESIAN_POINT('Ctrl Pts',(13.6807058074933,-0.335701785830877,
3.68856903744356));
#12883=CARTESIAN_POINT('Ctrl Pts',(13.6728344354434,-0.38702598691226,3.74389309969457));
#12884=CARTESIAN_POINT('Ctrl Pts',(13.6649630633934,-0.424383438206683,
3.81217413302386));
#12885=CARTESIAN_POINT('Ctrl Pts',(13.6570916913435,-0.443297653083863,
3.88523012494906));
#12886=CARTESIAN_POINT('Ctrl Pts',(13.6492203192935,-0.462211867961044,
3.95828611687427));
#12887=CARTESIAN_POINT('Ctrl Pts',(13.6413489472436,-0.462682846420982,
4.03611706739538));
#12888=CARTESIAN_POINT('Ctrl Pts',(13.6334775751936,-0.444654151830396,
4.10939661196244));
#12889=CARTESIAN_POINT('Ctrl Pts',(13.6256062031436,-0.42662545723981,4.18267615652949));
#12890=CARTESIAN_POINT('Ctrl Pts',(13.6177348310937,-0.3900970895987,4.25140429514248));
#12891=CARTESIAN_POINT('Ctrl Pts',(13.6098634590437,-0.339446187702822,
4.3073454393722));
#12892=CARTESIAN_POINT('Ctrl Pts',(13.6019920869938,-0.288795285806945,
4.36328658360191));
#12893=CARTESIAN_POINT('Ctrl Pts',(13.5941207149438,-0.224021849656302,
4.40644073344835));
#12894=CARTESIAN_POINT('Ctrl Pts',(13.5862493428939,-0.152887581692542,
4.43163679270085));
#12895=CARTESIAN_POINT('Ctrl Pts',(13.5808314647576,-0.103925749791867,
4.44897928111035));
#12896=CARTESIAN_POINT('Ctrl Pts',(13.5754135866214,-0.0519504158054226,
4.45781396031326));
#12897=CARTESIAN_POINT('Ctrl Pts',(13.5699957084852,1.03170790782398E-5,
4.4578580083501));
#12898=CARTESIAN_POINT('Ctrl Pts',(13.6800042915148,-8.85210990424201E-6,
4.45789764648838));
#12899=CARTESIAN_POINT('Ctrl Pts',(13.6810538713459,-0.010072447664127,
4.45790653275371));
#12900=CARTESIAN_POINT('Ctrl Pts',(13.6821034511769,-0.0201354698749596,
4.45758141170421));
#12901=CARTESIAN_POINT('Ctrl Pts',(13.683153031008,-0.0301761699425476,
4.45691829561871));
#12902=CARTESIAN_POINT('Ctrl Pts',(13.691024403058,-0.105476860309351,4.45194522614199));
#12903=CARTESIAN_POINT('Ctrl Pts',(13.6988957751079,-0.179522082183268,
4.42796223840642));
#12904=CARTESIAN_POINT('Ctrl Pts',(13.7067671471579,-0.24343910912634,4.38784317739428));
#12905=CARTESIAN_POINT('Ctrl Pts',(13.7146385192078,-0.307356136069411,
4.34772411638213));
#12906=CARTESIAN_POINT('Ctrl Pts',(13.7225098912578,-0.361144968081636,
4.2914689820934));
#12907=CARTESIAN_POINT('Ctrl Pts',(13.7303812633077,-0.398360171146024,
4.22581874179975));
#12908=CARTESIAN_POINT('Ctrl Pts',(13.7382526353577,-0.435575374210412,
4.1601685015061));
#12909=CARTESIAN_POINT('Ctrl Pts',(13.7461240074077,-0.456216948326962,
4.08512315520753));
#12910=CARTESIAN_POINT('Ctrl Pts',(13.7539953794576,-0.457811445030669,
4.00967527273228));
#12911=CARTESIAN_POINT('Ctrl Pts',(13.7618667515076,-0.459405941734377,
3.93422739025703));
#12912=CARTESIAN_POINT('Ctrl Pts',(13.7697381235575,-0.441953361025241,
3.85837697160509));
#12913=CARTESIAN_POINT('Ctrl Pts',(13.7776094956075,-0.407545019133394,
3.79121305720166));
#12914=CARTESIAN_POINT('Ctrl Pts',(13.7854808676574,-0.373136677241547,
3.72404914279823));
#12915=CARTESIAN_POINT('Ctrl Pts',(13.7933522397074,-0.321772574166988,
3.6655717326433));
#12916=CARTESIAN_POINT('Ctrl Pts',(13.8012236117573,-0.259607592342073,
3.6227880859492));
#12917=CARTESIAN_POINT('Ctrl Pts',(13.8090949838073,-0.19744261051716,3.5800044392551));
#12918=CARTESIAN_POINT('Ctrl Pts',(13.8169663558573,-0.124476749941891,
3.55291455602183));
#12919=CARTESIAN_POINT('Ctrl Pts',(13.8248377279072,-0.0494533988297167,
3.54476457579874));
#12920=CARTESIAN_POINT('Ctrl Pts',(13.8327090999572,0.0255699522824598,
3.53661459557564));
#12921=CARTESIAN_POINT('Ctrl Pts',(13.8405804720071,0.102650793931542,3.54740451836272));
#12922=CARTESIAN_POINT('Ctrl Pts',(13.8484518440571,0.172552645974024,3.57584140410587));
#12923=CARTESIAN_POINT('Ctrl Pts',(13.856323216107,0.242454498016503,3.60427828984902));
#12924=CARTESIAN_POINT('Ctrl Pts',(13.864194588157,0.305177360452382,3.65036213854823));
#12925=CARTESIAN_POINT('Ctrl Pts',(13.8720659602069,0.353205247972751,3.70857079263049));
#12926=CARTESIAN_POINT('Ctrl Pts',(13.8799373322569,0.40123313549312,3.76677944671275));
#12927=CARTESIAN_POINT('Ctrl Pts',(13.8878087043068,0.434566048097978,3.83711290617806));
#12928=CARTESIAN_POINT('Ctrl Pts',(13.8956800763568,0.44920975351361,3.9111432194385));
#12929=CARTESIAN_POINT('Ctrl Pts',(13.9035514484068,0.463853458929242,3.98517353269893));
#12930=CARTESIAN_POINT('Ctrl Pts',(13.9114228204567,0.459807957155645,4.06290069975448));
#12931=CARTESIAN_POINT('Ctrl Pts',(13.9192941925067,0.437558014523894,4.13501079227018));
#12932=CARTESIAN_POINT('Ctrl Pts',(13.9271655645566,0.415308071892144,4.20712088478587));
#12933=CARTESIAN_POINT('Ctrl Pts',(13.9350369366066,0.374853688402242,4.27361390276169));
#12934=CARTESIAN_POINT('Ctrl Pts',(13.9429083086565,0.321042451364188,4.32652208887851));
#12935=CARTESIAN_POINT('Ctrl Pts',(13.9507796807065,0.267231214326134,4.37943027499533));
#12936=CARTESIAN_POINT('Ctrl Pts',(13.9586510527564,0.200063123739928,4.41875362925314));
#12937=CARTESIAN_POINT('Ctrl Pts',(13.9665224248064,0.127586829849962,4.43978009385641));
#12938=CARTESIAN_POINT('Ctrl Pts',(13.9710163803759,0.086208370984788,4.45178460807712));
#12939=CARTESIAN_POINT('Ctrl Pts',(13.9755103359454,0.0430996806131821,
4.45782517307841));
#12940=CARTESIAN_POINT('Ctrl Pts',(13.9800042915148,-4.68615130337092E-6,
4.45784092071359));
#12941=CARTESIAN_POINT('Origin',(12.5,0.,4.));
#12942=CARTESIAN_POINT('',(14.2800042915148,1.11332528513013E-5,4.45786561359635));
#12943=CARTESIAN_POINT('',(14.1699957084852,-1.10604184835328E-5,4.4578646218584));
#12944=CARTESIAN_POINT('',(12.5,-5.60735153159594E-17,4.457875));
#12945=CARTESIAN_POINT('Ctrl Pts',(14.1699957084852,-1.10604184835328E-5,
4.4578646218584));
#12946=CARTESIAN_POINT('Ctrl Pts',(14.1643265158203,0.0543576752587709,
4.45781404039958));
#12947=CARTESIAN_POINT('Ctrl Pts',(14.1586573231555,0.108743966382031,4.44812254260427));
#12948=CARTESIAN_POINT('Ctrl Pts',(14.1529881304907,0.159684023833442,4.42916890146099));
#12949=CARTESIAN_POINT('Ctrl Pts',(14.1451167584407,0.230411580321883,4.40285278028461));
#12950=CARTESIAN_POINT('Ctrl Pts',(14.1372453863907,0.294495541512382,4.358681244225));
#12951=CARTESIAN_POINT('Ctrl Pts',(14.1293740143408,0.344256823700223,4.30194730133701));
#12952=CARTESIAN_POINT('Ctrl Pts',(14.1215026422908,0.394018105888063,4.24521335844902));
#12953=CARTESIAN_POINT('Ctrl Pts',(14.1136312702409,0.429456709073245,4.17591700873265));
#12954=CARTESIAN_POINT('Ctrl Pts',(14.1057598981909,0.446326079279053,4.10236192849032));
#12955=CARTESIAN_POINT('Ctrl Pts',(14.097888526141,0.46319544948486,4.02880684824799));
#12956=CARTESIAN_POINT('Ctrl Pts',(14.090017154091,0.461495586711293,3.95099303747972));
#12957=CARTESIAN_POINT('Ctrl Pts',(14.0821457820411,0.441430182931853,3.87824480690492));
#12958=CARTESIAN_POINT('Ctrl Pts',(14.0742744099911,0.421364779152413,3.80549657633012));
#12959=CARTESIAN_POINT('Ctrl Pts',(14.0664030379411,0.3829338343671,3.73781392594881));
#12960=CARTESIAN_POINT('Ctrl Pts',(14.0585316658912,0.330742470300218,3.68330716492384));
#12961=CARTESIAN_POINT('Ctrl Pts',(14.0506602938412,0.278551106233337,3.62880040389886));
#12962=CARTESIAN_POINT('Ctrl Pts',(14.0427889217913,0.212599322884887,3.58746953223022));
#12963=CARTESIAN_POINT('Ctrl Pts',(14.0349175497413,0.140790022250932,3.5642671654747));
#12964=CARTESIAN_POINT('Ctrl Pts',(14.0270461776914,0.0689807216169763,
3.54106479871918));
#12965=CARTESIAN_POINT('Ctrl Pts',(14.0191748056414,-0.00868609630248519,
3.53599093687678));
#12966=CARTESIAN_POINT('Ctrl Pts',(14.0113034335915,-0.0829037347177578,
3.5496535731032));
#12967=CARTESIAN_POINT('Ctrl Pts',(14.0034320615415,-0.15712137313303,3.56331620932962));
#12968=CARTESIAN_POINT('Ctrl Pts',(13.9955606894916,-0.227889832044114,
3.59571534362485));
#12969=CARTESIAN_POINT('Ctrl Pts',(13.9876893174416,-0.286729034540398,
3.64296863695132));
#12970=CARTESIAN_POINT('Ctrl Pts',(13.9798179453916,-0.345568237036683,
3.69022193027778));
#12971=CARTESIAN_POINT('Ctrl Pts',(13.9719465733417,-0.392478183118168,
3.75232938263547));
#12972=CARTESIAN_POINT('Ctrl Pts',(13.9640752012917,-0.421837725217638,
3.82184875237013));
#12973=CARTESIAN_POINT('Ctrl Pts',(13.9562038292418,-0.451197267317109,
3.8913681221048));
#12974=CARTESIAN_POINT('Ctrl Pts',(13.9483324571918,-0.463006405434566,
3.96829940921644));
#12975=CARTESIAN_POINT('Ctrl Pts',(13.9404610851419,-0.455850068491383,
4.04342405445454));
#12976=CARTESIAN_POINT('Ctrl Pts',(13.9325897130919,-0.448693731548199,
4.11854869969265));
#12977=CARTESIAN_POINT('Ctrl Pts',(13.924718341042,-0.422571919544373,4.19186670305722));
#12978=CARTESIAN_POINT('Ctrl Pts',(13.916846968992,-0.38061476952465,4.25459247959939));
#12979=CARTESIAN_POINT('Ctrl Pts',(13.908975596942,-0.338657619504927,4.31731825614156));
#12980=CARTESIAN_POINT('Ctrl Pts',(13.9011042248921,-0.280865131469307,
4.36945180586132));
#12981=CARTESIAN_POINT('Ctrl Pts',(13.8932328528421,-0.214162491453186,
4.40474604470388));
#12982=CARTESIAN_POINT('Ctrl Pts',(13.8854871380565,-0.148524681204106,
4.43947685223224));
#12983=CARTESIAN_POINT('Ctrl Pts',(13.8777414232708,-0.0742589286223064,
4.45790169736071));
#12984=CARTESIAN_POINT('Ctrl Pts',(13.8699957084852,1.23414887176878E-6,
4.4579133809027));
#12985=CARTESIAN_POINT('Ctrl Pts',(13.9800042915148,-4.68615130337092E-6,
4.45784092071359));
#12986=CARTESIAN_POINT('Ctrl Pts',(13.9833817079953,-0.0323996211791616,
4.45785275579335));
#12987=CARTESIAN_POINT('Ctrl Pts',(13.9867591244758,-0.064792114138131,
4.45446164082457));
#12988=CARTESIAN_POINT('Ctrl Pts',(13.9901365409563,-0.0964458636128916,
4.44764173788363));
#12989=CARTESIAN_POINT('Ctrl Pts',(13.9980079130062,-0.170217765992045,
4.43174734235885));
#12990=CARTESIAN_POINT('Ctrl Pts',(14.0058792850562,-0.239977073556624,
4.39722897636055));
#12991=CARTESIAN_POINT('Ctrl Pts',(14.0137506571061,-0.297364634468633,
4.34822292324149));
#12992=CARTESIAN_POINT('Ctrl Pts',(14.0216220291561,-0.354752195380644,
4.29921687012243));
#12993=CARTESIAN_POINT('Ctrl Pts',(14.0294934012061,-0.399768009640084,
4.23572312988262));
#12994=CARTESIAN_POINT('Ctrl Pts',(14.037364773256,-0.427017900618165,4.16535006094698));
#12995=CARTESIAN_POINT('Ctrl Pts',(14.045236145306,-0.454267791596245,4.09497699201134));
#12996=CARTESIAN_POINT('Ctrl Pts',(14.0531075173559,-0.463751759292965,
4.01772459437987));
#12997=CARTESIAN_POINT('Ctrl Pts',(14.0609788894059,-0.45433335426851,3.94284990548881));
#12998=CARTESIAN_POINT('Ctrl Pts',(14.0688502614558,-0.444914949244056,
3.86797521659775));
#12999=CARTESIAN_POINT('Ctrl Pts',(14.0767216335058,-0.416594171498428,
3.7954782364471));
#13000=CARTESIAN_POINT('Ctrl Pts',(14.0845930055557,-0.372764656800254,
3.7340461680214));
#13001=CARTESIAN_POINT('Ctrl Pts',(14.0924643776057,-0.328935142102078,
3.67261409959569));
#13002=CARTESIAN_POINT('Ctrl Pts',(14.1003357496557,-0.269596890451354,
3.62224694289495));
#13003=CARTESIAN_POINT('Ctrl Pts',(14.1082071217056,-0.201860314388951,
3.58898011778223));
#13004=CARTESIAN_POINT('Ctrl Pts',(14.1160784937556,-0.134123738326549,
3.55571329266952));
#13005=CARTESIAN_POINT('Ctrl Pts',(14.1239498658055,-0.0579888378524715,
3.53954679914483));
#13006=CARTESIAN_POINT('Ctrl Pts',(14.1318212378555,0.0174212575835846,
3.54241784356498));
#13007=CARTESIAN_POINT('Ctrl Pts',(14.1396926099054,0.0928313530196406,
3.54528888798513));
#13008=CARTESIAN_POINT('Ctrl Pts',(14.1475639819554,0.167516643417675,3.56719747035013));
#13009=CARTESIAN_POINT('Ctrl Pts',(14.1554353540053,0.232527703900953,3.60551831852155));
#13010=CARTESIAN_POINT('Ctrl Pts',(14.1633067260553,0.297538764384231,3.64383916669297));
#13011=CARTESIAN_POINT('Ctrl Pts',(14.1711780981053,0.352875594952755,3.69857228067082));
#13012=CARTESIAN_POINT('Ctrl Pts',(14.1790494701552,0.391907267274456,3.76315907456484));
#13013=CARTESIAN_POINT('Ctrl Pts',(14.1869208422052,0.430938939596158,3.82774586845886));
#13014=CARTESIAN_POINT('Ctrl Pts',(14.1947922142551,0.453665453671035,3.90218634226906));
#13015=CARTESIAN_POINT('Ctrl Pts',(14.2026635863051,0.45736352584659,3.97756040711846));
#13016=CARTESIAN_POINT('Ctrl Pts',(14.210534958355,0.461061598022145,4.05293447196787));
#13017=CARTESIAN_POINT('Ctrl Pts',(14.218406330405,0.445731228298378,4.12924212785648));
#13018=CARTESIAN_POINT('Ctrl Pts',(14.2262777024549,0.413209431587385,4.19733954431574));
#13019=CARTESIAN_POINT('Ctrl Pts',(14.2341490745049,0.380687634876391,4.265436960775));
#13020=CARTESIAN_POINT('Ctrl Pts',(14.2420204465549,0.330974411178171,4.32532413780492));
#13021=CARTESIAN_POINT('Ctrl Pts',(14.2498918186048,0.270026820557645,4.36982488597043));
#13022=CARTESIAN_POINT('Ctrl Pts',(14.2577631906548,0.209079229937118,4.41432563413594));
#13023=CARTESIAN_POINT('Ctrl Pts',(14.2656345627047,0.136897272394287,4.44343995343705));
#13024=CARTESIAN_POINT('Ctrl Pts',(14.2735059347547,0.0621304022332317,
4.45367911922619));
#13025=CARTESIAN_POINT('Ctrl Pts',(14.2756720536747,0.0415553447945806,
4.4564968301158));
#13026=CARTESIAN_POINT('Ctrl Pts',(14.2778381725948,0.020784533837212,4.45788513960506));
#13027=CARTESIAN_POINT('Ctrl Pts',(14.2800042915148,1.11332528513013E-5,
4.45786561359635));
#13028=CARTESIAN_POINT('Origin',(12.5,0.,4.));
#13029=CARTESIAN_POINT('',(14.5800042915148,-1.58578451148518E-6,4.45791318879952));
#13030=CARTESIAN_POINT('',(14.4699957084852,4.96934848862042E-6,4.4578413260902));
#13031=CARTESIAN_POINT('',(12.5,-5.60735153159594E-17,4.457875));
#13032=CARTESIAN_POINT('Ctrl Pts',(14.4699957084852,4.96934848862042E-6,
4.4578413260902));
#13033=CARTESIAN_POINT('Ctrl Pts',(14.4666543524698,0.0320539454002899,
4.45785375637851));
#13034=CARTESIAN_POINT('Ctrl Pts',(14.4633129964543,0.0641003838712636,
4.45453523052653));
#13035=CARTESIAN_POINT('Ctrl Pts',(14.4599716404389,0.0954313752779353,
4.44785911407655));
#13036=CARTESIAN_POINT('Ctrl Pts',(14.452100268389,0.169239101517837,4.43213190746217));
#13037=CARTESIAN_POINT('Ctrl Pts',(14.444228896339,0.2390764403586,4.39777168651743));
#13038=CARTESIAN_POINT('Ctrl Pts',(14.4363575242891,0.296574889592956,4.34889578431359));
#13039=CARTESIAN_POINT('Ctrl Pts',(14.4284861522391,0.354073338827311,4.30001988210975));
#13040=CARTESIAN_POINT('Ctrl Pts',(14.4206147801891,0.39923289845526,4.2366282986468));
#13041=CARTESIAN_POINT('Ctrl Pts',(14.4127434081392,0.4266421670589,4.16631715105832));
#13042=CARTESIAN_POINT('Ctrl Pts',(14.4048720360892,0.454051435662541,4.09600600346984));
#13043=CARTESIAN_POINT('Ctrl Pts',(14.3970006640393,0.463710413241873,4.01877529175582));
#13044=CARTESIAN_POINT('Ctrl Pts',(14.3891292919893,0.454461679188747,3.94387945476197));
#13045=CARTESIAN_POINT('Ctrl Pts',(14.3812579199394,0.445212945135621,3.86898361776811));
#13046=CARTESIAN_POINT('Ctrl Pts',(14.3733865478894,0.417056499450037,3.79642265549441));
#13047=CARTESIAN_POINT('Ctrl Pts',(14.3655151758395,0.373366286239542,3.73489143780602));
#13048=CARTESIAN_POINT('Ctrl Pts',(14.3576438037895,0.329676073029047,3.67336022011762));
#13049=CARTESIAN_POINT('Ctrl Pts',(14.3497724317395,0.270452092293641,3.62285874701452));
#13050=CARTESIAN_POINT('Ctrl Pts',(14.3419010596896,0.202791063664024,3.58943853329022));
#13051=CARTESIAN_POINT('Ctrl Pts',(14.3340296876396,0.135130035034407,3.55601831956592));
#13052=CARTESIAN_POINT('Ctrl Pts',(14.3261583155897,0.0590319585105798,
3.53967936522043));
#13053=CARTESIAN_POINT('Ctrl Pts',(14.3182869435397,-0.0163844490157649,
3.54237954232867));
#13054=CARTESIAN_POINT('Ctrl Pts',(14.3104155714898,-0.0918008565421096,
3.54507971943691));
#13055=CARTESIAN_POINT('Ctrl Pts',(14.3025441994398,-0.166535595070972,
3.56681902799889));
#13056=CARTESIAN_POINT('Ctrl Pts',(14.2946728273899,-0.231633314431234,
3.60499247969884));
#13057=CARTESIAN_POINT('Ctrl Pts',(14.2868014553399,-0.296731033791496,
3.64316593139879));
#13058=CARTESIAN_POINT('Ctrl Pts',(14.2789300832899,-0.352191733983158,
3.6977735262367));
#13059=CARTESIAN_POINT('Ctrl Pts',(14.27105871124,-0.391369643565407,3.76227171909014));
#13060=CARTESIAN_POINT('Ctrl Pts',(14.26318733919,-0.430547553147657,3.82676991194359));
#13061=CARTESIAN_POINT('Ctrl Pts',(14.2553159671401,-0.453442672120494,
3.90115870281258));
#13062=CARTESIAN_POINT('Ctrl Pts',(14.2474445950901,-0.457311513162664,
3.97652419590847));
#13063=CARTESIAN_POINT('Ctrl Pts',(14.2395732230402,-0.461180354204834,
4.05188968900435));
#13064=CARTESIAN_POINT('Ctrl Pts',(14.2317018509902,-0.446022917316338,
4.12823188432714));
#13065=CARTESIAN_POINT('Ctrl Pts',(14.2238304789403,-0.413655495130362,
4.19640281260034));
#13066=CARTESIAN_POINT('Ctrl Pts',(14.2159591068903,-0.381288072944386,
4.26457374087354));
#13067=CARTESIAN_POINT('Ctrl Pts',(14.2080877348403,-0.33171066546093,4.32457340209717));
#13068=CARTESIAN_POINT('Ctrl Pts',(14.2002163627904,-0.270864058094251,
4.36921212802613));
#13069=CARTESIAN_POINT('Ctrl Pts',(14.1923449907404,-0.210017450727571,
4.41385085395509));
#13070=CARTESIAN_POINT('Ctrl Pts',(14.1844736186905,-0.137901643477669,
4.44312864458938));
#13071=CARTESIAN_POINT('Ctrl Pts',(14.1766022466405,-0.0631581639595259,
4.45353718675995));
#13072=CARTESIAN_POINT('Ctrl Pts',(14.1744000672554,-0.0422471272657682,
4.45644919204336));
#13073=CARTESIAN_POINT('Ctrl Pts',(14.1721978878703,-0.021130418320356,
4.45788427006097));
#13074=CARTESIAN_POINT('Ctrl Pts',(14.1699957084852,-1.10604184835328E-5,
4.4578646218584));
#13075=CARTESIAN_POINT('Ctrl Pts',(14.2800042915148,1.11332528513013E-5,
4.45786561359635));
#13076=CARTESIAN_POINT('Ctrl Pts',(14.2857095446447,-0.0547030874695854,
4.45781418483069));
#13077=CARTESIAN_POINT('Ctrl Pts',(14.2914147977746,-0.109435272994953,
4.44799629651036));
#13078=CARTESIAN_POINT('Ctrl Pts',(14.2971200509045,-0.16065599949712,4.42880599334559));
#13079=CARTESIAN_POINT('Ctrl Pts',(14.3049914229545,-0.231323748287136,
4.40232968939868));
#13080=CARTESIAN_POINT('Ctrl Pts',(14.3128627950045,-0.295307463087888,
4.35801306922771));
#13081=CARTESIAN_POINT('Ctrl Pts',(14.3207341670544,-0.344940072567234,
4.30116652609615));
#13082=CARTESIAN_POINT('Ctrl Pts',(14.3286055391044,-0.394572682046581,
4.24431998296459));
#13083=CARTESIAN_POINT('Ctrl Pts',(14.3364769111543,-0.429854186204522,
4.17494351687244));
#13084=CARTESIAN_POINT('Ctrl Pts',(14.3443482832043,-0.446556856002091,
4.10135040434572));
#13085=CARTESIAN_POINT('Ctrl Pts',(14.3522196552542,-0.46325952579966,4.027757291819));
#13086=CARTESIAN_POINT('Ctrl Pts',(14.3600910273042,-0.461383361236856,
3.9499475328577));
#13087=CARTESIAN_POINT('Ctrl Pts',(14.3679623993541,-0.441153180262727,
3.87724495265939));
#13088=CARTESIAN_POINT('Ctrl Pts',(14.3758337714041,-0.420922999288597,
3.80454237246108));
#13089=CARTESIAN_POINT('Ctrl Pts',(14.383705143454,-0.382338801903142,3.73694697102576));
#13090=CARTESIAN_POINT('Ctrl Pts',(14.391576515504,-0.330024073856894,3.68255860260764));
#13091=CARTESIAN_POINT('Ctrl Pts',(14.399447887554,-0.277709345810648,3.62817023418952));
#13092=CARTESIAN_POINT('Ctrl Pts',(14.4073192596039,-0.21166408710361,3.58698889878861));
#13093=CARTESIAN_POINT('Ctrl Pts',(14.4151906316539,-0.139802400742051,
3.56394929325792));
#13094=CARTESIAN_POINT('Ctrl Pts',(14.4230620037038,-0.0679407143804897,
3.54090968772722));
#13095=CARTESIAN_POINT('Ctrl Pts',(14.4309333757538,0.00973739963559066,
3.53601181206673));
#13096=CARTESIAN_POINT('Ctrl Pts',(14.4388047478037,0.0839238909224197,
3.54984257127538));
#13097=CARTESIAN_POINT('Ctrl Pts',(14.4466761198537,0.158110382209248,3.56367333048403));
#13098=CARTESIAN_POINT('Ctrl Pts',(14.4545474919037,0.228805250766822,3.59623272456181));
#13099=CARTESIAN_POINT('Ctrl Pts',(14.4624188639536,0.287537237904754,3.64361921078484));
#13100=CARTESIAN_POINT('Ctrl Pts',(14.4702902360036,0.346269225042686,3.69100569700788));
#13101=CARTESIAN_POINT('Ctrl Pts',(14.4781616080535,0.393038330760977,3.75321927537615));
#13102=CARTESIAN_POINT('Ctrl Pts',(14.4860329801035,0.422240284179214,3.8228049873169));
#13103=CARTESIAN_POINT('Ctrl Pts',(14.4939043521534,0.451442237597453,3.89239069925764));
#13104=CARTESIAN_POINT('Ctrl Pts',(14.5017757242034,0.463077038715637,3.96934854477086));
#13105=CARTESIAN_POINT('Ctrl Pts',(14.5096470962533,0.45575050699275,4.04445678215295));
#13106=CARTESIAN_POINT('Ctrl Pts',(14.5175184683033,0.448423975269863,4.11956501953505));
#13107=CARTESIAN_POINT('Ctrl Pts',(14.5253898403532,0.422136110705906,4.19282364878603));
#13108=CARTESIAN_POINT('Ctrl Pts',(14.5332612124032,0.380036948171907,4.2554541996672));
#13109=CARTESIAN_POINT('Ctrl Pts',(14.5411325844532,0.337937785637909,4.31808475054837));
#13110=CARTESIAN_POINT('Ctrl Pts',(14.5490039565031,0.28002732513387,4.37008722305972));
#13111=CARTESIAN_POINT('Ctrl Pts',(14.5568753285531,0.213244889156206,4.40523023992844));
#13112=CARTESIAN_POINT('Ctrl Pts',(14.5645849828737,0.147834501639678,4.43965124177167));
#13113=CARTESIAN_POINT('Ctrl Pts',(14.5722946371942,0.0739129441497101,
4.45789842831743));
#13114=CARTESIAN_POINT('Ctrl Pts',(14.5800042915148,-1.58578451148518E-6,
4.45791318879952));
#13115=CARTESIAN_POINT('Origin',(12.5,0.,4.));
#13116=CARTESIAN_POINT('',(14.8800042915148,-1.01702808208336E-5,4.45785711824254));
#13117=CARTESIAN_POINT('',(14.7699957084852,8.6346448269735E-6,4.45789857801605));
#13118=CARTESIAN_POINT('',(12.5,-5.60735153159594E-17,4.457875));
#13119=CARTESIAN_POINT('Ctrl Pts',(14.7699957084852,8.6346448269735E-6,
4.45789857801605));
#13120=CARTESIAN_POINT('Ctrl Pts',(14.7689821891192,0.00972641784825355,
4.45790700998655));
#13121=CARTESIAN_POINT('Ctrl Pts',(14.7679686697532,0.01944367562558,4.45760386164098));
#13122=CARTESIAN_POINT('Ctrl Pts',(14.7669551503872,0.0291408329004781,
4.45698549795522));
#13123=CARTESIAN_POINT('Ctrl Pts',(14.7590837783372,0.104452598317788,4.45218305332902));
#13124=CARTESIAN_POINT('Ctrl Pts',(14.7512124062873,0.178551969979598,4.4283678943965));
#13125=CARTESIAN_POINT('Ctrl Pts',(14.7433410342373,0.242559732875008,4.38839375563686));
#13126=CARTESIAN_POINT('Ctrl Pts',(14.7354696621874,0.30656749577042,4.34841961687722));
#13127=CARTESIAN_POINT('Ctrl Pts',(14.7275982901374,0.360483649899433,4.29228649829047));
#13128=CARTESIAN_POINT('Ctrl Pts',(14.7197269180875,0.397847504376097,4.22672074611392));
#13129=CARTESIAN_POINT('Ctrl Pts',(14.7118555460375,0.435211358852761,4.16115499393738));
#13130=CARTESIAN_POINT('Ctrl Pts',(14.7039841739875,0.456022913677073,4.08615660817103));
#13131=CARTESIAN_POINT('Ctrl Pts',(14.6961128019376,0.457788351878884,4.01071253147039));
#13132=CARTESIAN_POINT('Ctrl Pts',(14.6882414298876,0.459553790080695,3.93526845476975));
#13133=CARTESIAN_POINT('Ctrl Pts',(14.6803700578377,0.442273111660005,3.85937868713481));
#13134=CARTESIAN_POINT('Ctrl Pts',(14.6724986857877,0.408017034045316,3.79213698410258));
#13135=CARTESIAN_POINT('Ctrl Pts',(14.6646273137378,0.373760956430627,3.72489528107034));
#13136=CARTESIAN_POINT('Ctrl Pts',(14.6567559416878,0.32252947962194,3.6663016426408));
#13137=CARTESIAN_POINT('Ctrl Pts',(14.6488845696379,0.260461593653079,3.6233772554918));
#13138=CARTESIAN_POINT('Ctrl Pts',(14.6410131975879,0.198393707684219,3.5804528683428));
#13139=CARTESIAN_POINT('Ctrl Pts',(14.6331418255379,0.125489412555185,3.55319773247434));
#13140=CARTESIAN_POINT('Ctrl Pts',(14.625270453488,0.0504847191830214,3.54487778940425));
#13141=CARTESIAN_POINT('Ctrl Pts',(14.617399081438,-0.0245199741891427,
3.53655784633416));
#13142=CARTESIAN_POINT('Ctrl Pts',(14.6095277093881,-0.101625065804437,
3.54717309606245));
#13143=CARTESIAN_POINT('Ctrl Pts',(14.6016563373381,-0.171591169681571,
3.57545152934398));
#13144=CARTESIAN_POINT('Ctrl Pts',(14.5937849652882,-0.241557273558703,
3.6037299626255));
#13145=CARTESIAN_POINT('Ctrl Pts',(14.5859135932382,-0.304384389697674,
3.64967157946028));
#13146=CARTESIAN_POINT('Ctrl Pts',(14.5780422211883,-0.352544040227279,
3.70777126570269));
#13147=CARTESIAN_POINT('Ctrl Pts',(14.5701708491383,-0.400703690756885,
3.7658709519451));
#13148=CARTESIAN_POINT('Ctrl Pts',(14.5622994770883,-0.434195875677124,
3.83612870759516));
#13149=CARTESIAN_POINT('Ctrl Pts',(14.5544281050384,-0.449007277354457,
3.91012565253846));
#13150=CARTESIAN_POINT('Ctrl Pts',(14.5465567329884,-0.46381867903179,3.98412259748177));
#13151=CARTESIAN_POINT('Ctrl Pts',(14.5386853609385,-0.459949297466218,
4.06185873171832));
#13152=CARTESIAN_POINT('Ctrl Pts',(14.5308139888885,-0.437862794771992,
4.13401905238929));
#13153=CARTESIAN_POINT('Ctrl Pts',(14.5229426168386,-0.415776292077766,
4.20617937306026));
#13154=CARTESIAN_POINT('Ctrl Pts',(14.5150712447886,-0.375472668254887,
4.27276388016565));
#13155=CARTESIAN_POINT('Ctrl Pts',(14.5071998727387,-0.321781445311454,
4.32579385338299));
#13156=CARTESIAN_POINT('Ctrl Pts',(14.4993285006887,-0.26809022236802,4.37882382660034));
#13157=CARTESIAN_POINT('Ctrl Pts',(14.4914571286387,-0.201011400304033,
4.41829926592964));
#13158=CARTESIAN_POINT('Ctrl Pts',(14.4835857565888,-0.128582932452519,
4.43948988945229));
#13159=CARTESIAN_POINT('Ctrl Pts',(14.4790557405542,-0.0868999680795747,
4.45168520479633));
#13160=CARTESIAN_POINT('Ctrl Pts',(14.4745257245197,-0.0434451672832877,
4.45782447382869));
#13161=CARTESIAN_POINT('Ctrl Pts',(14.4699957084852,4.96934848862042E-6,
4.4578413260902));
#13162=CARTESIAN_POINT('Ctrl Pts',(14.5800042915148,-1.58578451148518E-6,
4.45791318879952));
#13163=CARTESIAN_POINT('Ctrl Pts',(14.5801660092442,-0.00155201715944126,
4.45791349841543));
#13164=CARTESIAN_POINT('Ctrl Pts',(14.5803277269736,-0.00310244544229786,
4.45790578589721));
#13165=CARTESIAN_POINT('Ctrl Pts',(14.5804894447029,-0.0046527920161852,
4.45789003224535));
#13166=CARTESIAN_POINT('Ctrl Pts',(14.5883608167529,-0.0801136257596197,
4.45712324646747));
#13167=CARTESIAN_POINT('Ctrl Pts',(14.5962321888029,-0.155380881795201,
4.43730611368561));
#13168=CARTESIAN_POINT('Ctrl Pts',(14.6041035608528,-0.22143539919095,4.4008132908088));
#13169=CARTESIAN_POINT('Ctrl Pts',(14.6119749329028,-0.287489916586699,
4.36432046793199));
#13170=CARTESIAN_POINT('Ctrl Pts',(14.6198463049527,-0.344331695342615,
4.31115195496024));
#13171=CARTESIAN_POINT('Ctrl Pts',(14.6277176770027,-0.38514947146564,4.24767885402976));
#13172=CARTESIAN_POINT('Ctrl Pts',(14.6355890490526,-0.425967247588666,
4.18420575309928));
#13173=CARTESIAN_POINT('Ctrl Pts',(14.6434604211026,-0.4507610210788,4.11042806421008));
#13174=CARTESIAN_POINT('Ctrl Pts',(14.6513317931525,-0.45655979174196,4.03518645571321));
#13175=CARTESIAN_POINT('Ctrl Pts',(14.6592031652025,-0.462358562405121,
3.95994484721634));
#13176=CARTESIAN_POINT('Ctrl Pts',(14.6670745372524,-0.449162330241309,
3.8832393191118));
#13177=CARTESIAN_POINT('Ctrl Pts',(14.6749459093024,-0.41855237967279,3.81426137832517));
#13178=CARTESIAN_POINT('Ctrl Pts',(14.6828172813524,-0.387942429104271,
3.74528343753854));
#13179=CARTESIAN_POINT('Ctrl Pts',(14.6906886534023,-0.339918760131043,
3.68403308406983));
#13180=CARTESIAN_POINT('Ctrl Pts',(14.6985600254523,-0.280235976103336,
3.63784985464301));
#13181=CARTESIAN_POINT('Ctrl Pts',(14.7064313975022,-0.220553192075631,
3.5916666252162));
#13182=CARTESIAN_POINT('Ctrl Pts',(14.7143027695522,-0.149211292993445,
3.5605505198313));
#13183=CARTESIAN_POINT('Ctrl Pts',(14.7221741416021,-0.0747590701011626,
3.54823013427646));
#13184=CARTESIAN_POINT('Ctrl Pts',(14.7300455136521,-0.000306847208877067,
3.53590974872161));
#13185=CARTESIAN_POINT('Ctrl Pts',(14.737916885702,0.0772556994935079,3.54238508299684));
#13186=CARTESIAN_POINT('Ctrl Pts',(14.745788257752,0.148634367597872,3.5668802073009));
#13187=CARTESIAN_POINT('Ctrl Pts',(14.753659629802,0.220013035702235,3.59137533160497));
#13188=CARTESIAN_POINT('Ctrl Pts',(14.7615310018519,0.285207825208577,3.63389024593787));
#13189=CARTESIAN_POINT('Ctrl Pts',(14.7694023739019,0.336406544142474,3.68933045342307));
#13190=CARTESIAN_POINT('Ctrl Pts',(14.7772737459518,0.387605263076371,3.74477066090827));
#13191=CARTESIAN_POINT('Ctrl Pts',(14.7851451180018,0.424807911437823,3.81313616154577));
#13192=CARTESIAN_POINT('Ctrl Pts',(14.7930164900517,0.443556551112275,3.88623481973509));
#13193=CARTESIAN_POINT('Ctrl Pts',(14.8008878621017,0.462305190786727,3.9593334779244));
#13194=CARTESIAN_POINT('Ctrl Pts',(14.8087592341516,0.462599821774179,4.03716529366552));
#13195=CARTESIAN_POINT('Ctrl Pts',(14.8166306062016,0.444405141642572,4.11040380200553));
#13196=CARTESIAN_POINT('Ctrl Pts',(14.8245019782516,0.426210461510966,4.18364231034555));
#13197=CARTESIAN_POINT('Ctrl Pts',(14.8323733503015,0.389526470260302,4.25228751128446));
#13198=CARTESIAN_POINT('Ctrl Pts',(14.8402447223515,0.338748948932789,4.3081137476731));
#13199=CARTESIAN_POINT('Ctrl Pts',(14.8481160944014,0.287971427605278,4.36393998406173));
#13200=CARTESIAN_POINT('Ctrl Pts',(14.8559874664514,0.22310037620092,4.40694725590009));
#13201=CARTESIAN_POINT('Ctrl Pts',(14.8638588385013,0.151909206873508,4.43198208217373));
#13202=CARTESIAN_POINT('Ctrl Pts',(14.8692406561725,0.103234351881841,4.44909890368578));
#13203=CARTESIAN_POINT('Ctrl Pts',(14.8746224738437,0.0516050086776526,
4.45781408155485));
#13204=CARTESIAN_POINT('Ctrl Pts',(14.8800042915148,-1.01702808208336E-5,
4.45785711824254));
#13205=CARTESIAN_POINT('Origin',(12.5,0.,4.));
#13206=CARTESIAN_POINT('',(15.1,-5.60735153159594E-17,4.457875));
#13207=CARTESIAN_POINT('',(15.0699957084852,-1.05870731373636E-5,4.45788944868556));
#13208=CARTESIAN_POINT('',(12.5,-5.60735153159594E-17,4.457875));
#13209=CARTESIAN_POINT('',(15.1,-0.269165465906718,4.37040446485999));
#13210=CARTESIAN_POINT('Origin',(15.1,0.,4.));
#13211=CARTESIAN_POINT('Ctrl Pts',(15.1,-0.269173508333955,4.37043259773194));
#13212=CARTESIAN_POINT('Ctrl Pts',(15.0991842588284,-0.262849866117432,
4.37503549456412));
#13213=CARTESIAN_POINT('Ctrl Pts',(15.0983685176569,-0.256407545646713,
4.37947450812006));
#13214=CARTESIAN_POINT('Ctrl Pts',(15.0975527764853,-0.249853611926923,
4.38374199825787));
#13215=CARTESIAN_POINT('Ctrl Pts',(15.0896814044354,-0.186612411779406,
4.42492050409441));
#13216=CARTESIAN_POINT('Ctrl Pts',(15.0818100323854,-0.112978907049287,
4.45012847221118));
#13217=CARTESIAN_POINT('Ctrl Pts',(15.0739386603355,-0.0377721395608013,
4.45635245505497));
#13218=CARTESIAN_POINT('Ctrl Pts',(15.072624343052,-0.0252145379490987,
4.45739170058566));
#13219=CARTESIAN_POINT('Ctrl Pts',(15.0713100257686,-0.0126130730861363,
4.45790166433459));
#13220=CARTESIAN_POINT('Ctrl Pts',(15.0699957084852,-1.05870731373636E-5,
4.45788944868556));
#13221=CARTESIAN_POINT('Origin',(11.8752146997001,0.,4.));
#13222=CARTESIAN_POINT('',(14.9247853002999,-1.38824472118437E-5,4.62497559137666));
#13223=CARTESIAN_POINT('',(15.0252146997001,-1.44513692928093E-5,4.62501972247551));
#13224=CARTESIAN_POINT('',(11.8752146997001,-1.68747709936658E-14,4.625));
#13225=CARTESIAN_POINT('',(15.1,-0.624993681275899,4.00281040303151));
#13226=CARTESIAN_POINT('Ctrl Pts',(15.0252146997001,-1.44513692928189E-5,
4.62501972247551));
#13227=CARTESIAN_POINT('Ctrl Pts',(15.0265290169835,-0.017216861979444,
4.62503639685311));
#13228=CARTESIAN_POINT('Ctrl Pts',(15.0357147063169,-0.137433797398843,
4.62017138475037));
#13229=CARTESIAN_POINT('Ctrl Pts',(15.0527717677003,-0.355236031271534,
4.54560815721762));
#13230=CARTESIAN_POINT('Ctrl Pts',(15.0763858838501,-0.571652475026301,
4.31158258982903));
#13231=CARTESIAN_POINT('Ctrl Pts',(15.09212862795,-0.624530364890795,4.10584538053252));
#13232=CARTESIAN_POINT('Ctrl Pts',(15.1,-0.624993681275899,4.00281040303152));
#13233=CARTESIAN_POINT('',(15.1,0.314930721058197,3.46014479632612));
#13234=CARTESIAN_POINT('Origin',(15.1,0.,4.));
#13235=CARTESIAN_POINT('Ctrl Pts',(14.9247853002999,-1.38824472118368E-5,
4.62497559137666));
#13236=CARTESIAN_POINT('Ctrl Pts',(14.9272748546787,-0.0326052931943186,
4.62500276606431));
#13237=CARTESIAN_POINT('Ctrl Pts',(14.9376357811074,-0.168225686180582,
4.61457389311938));
#13238=CARTESIAN_POINT('Ctrl Pts',(14.9558680795861,-0.394527586443172,
4.517903766532));
#13239=CARTESIAN_POINT('Ctrl Pts',(14.979482195736,-0.593077772790822,4.26857965265179));
#13240=CARTESIAN_POINT('Ctrl Pts',(15.0030963118859,-0.649493436571599,
3.95488773069898));
#13241=CARTESIAN_POINT('Ctrl Pts',(15.0267104280357,-0.550252000240565,
3.65200904506483));
#13242=CARTESIAN_POINT('Ctrl Pts',(15.0503245441856,-0.319142060764588,
3.43252503194012));
#13243=CARTESIAN_POINT('Ctrl Pts',(15.0739386603355,-0.0115409051696555,
3.34904846156061));
#13244=CARTESIAN_POINT('Ctrl Pts',(15.0904971456069,0.20608092381284,3.39989411918499));
#13245=CARTESIAN_POINT('Ctrl Pts',(15.0991842588284,0.305720220830039,3.45471854406458));
#13246=CARTESIAN_POINT('Ctrl Pts',(15.1,0.314937815442301,3.46010549098218));
#13247=CARTESIAN_POINT('Origin',(11.8752146997001,0.,4.));
#13248=CARTESIAN_POINT('',(14.6247853002999,-2.16459804047719E-6,4.62505212776347));
#13249=CARTESIAN_POINT('',(14.7252146997001,1.17863019661874E-5,4.62503218402409));
#13250=CARTESIAN_POINT('',(11.8752146997001,-1.68747709936658E-14,4.625));
#13251=CARTESIAN_POINT('Ctrl Pts',(14.7252146997001,1.17863019662174E-5,
4.62503218402409));
#13252=CARTESIAN_POINT('Ctrl Pts',(14.7320725523841,-0.0897427467603322,
4.62495430540108));
#13253=CARTESIAN_POINT('Ctrl Pts',(14.746801777118,-0.282587126126967,4.58296482291278));
#13254=CARTESIAN_POINT('Ctrl Pts',(14.7694023739019,-0.520130285395982,
4.39158760667368));
#13255=CARTESIAN_POINT('Ctrl Pts',(14.7930164900517,-0.64367318065081,4.09778141619902));
#13256=CARTESIAN_POINT('Ctrl Pts',(14.8166306062016,-0.612955311082805,
3.78054123783642));
#13257=CARTESIAN_POINT('Ctrl Pts',(14.8402447223515,-0.435338447621071,
3.51589585985611));
#13258=CARTESIAN_POINT('Ctrl Pts',(14.8638588385013,-0.153389665944836,
3.36726945127358));
#13259=CARTESIAN_POINT('Ctrl Pts',(14.8874729546512,0.165319955489652,3.37028123293502));
#13260=CARTESIAN_POINT('Ctrl Pts',(14.9110870708011,0.444409630539555,3.52420969451069));
#13261=CARTESIAN_POINT('Ctrl Pts',(14.9347011869509,0.616993161964042,3.79216419995926));
#13262=CARTESIAN_POINT('Ctrl Pts',(14.9583153031008,0.641710593195818,4.10992889087348));
#13263=CARTESIAN_POINT('Ctrl Pts',(14.9819294192507,0.512636325700993,4.40134645341462));
#13264=CARTESIAN_POINT('Ctrl Pts',(15.0042292181171,0.274729866520086,4.58571614948967));
#13265=CARTESIAN_POINT('Ctrl Pts',(15.0186576449336,0.0858074045169303,
4.62493653494651));
#13266=CARTESIAN_POINT('Ctrl Pts',(15.0252146997001,-1.44513692928189E-5,
4.62501972247551));
#13267=CARTESIAN_POINT('Ctrl Pts',(14.6247853002999,-2.16459804049194E-6,
4.62505212776347));
#13268=CARTESIAN_POINT('Ctrl Pts',(14.6249470180292,-0.00211850554115318,
4.62505255038961));
#13269=CARTESIAN_POINT('Ctrl Pts',(14.6329801078086,-0.107244412024774,
4.62452960748548));
#13270=CARTESIAN_POINT('Ctrl Pts',(14.6488845696379,-0.314835022974042,
4.56987302880665));
#13271=CARTESIAN_POINT('Ctrl Pts',(14.6724986857877,-0.547602339746838,
4.35214775046202));
#13272=CARTESIAN_POINT('Ctrl Pts',(14.6961128019376,-0.649132943719538,
4.05002781234082));
#13273=CARTESIAN_POINT('Ctrl Pts',(14.7197269180875,-0.595094318970103,
3.73591836064326));
#13274=CARTESIAN_POINT('Ctrl Pts',(14.7433410342373,-0.398437197867616,
3.48509791236843));
#13275=CARTESIAN_POINT('Ctrl Pts',(14.7669551503872,-0.1062918289807,3.35767733339665));
#13276=CARTESIAN_POINT('Ctrl Pts',(14.7905692665371,0.211327117384507,3.38419385377023));
#13277=CARTESIAN_POINT('Ctrl Pts',(14.8141833826869,0.478300047385911,3.5582926020622));
#13278=CARTESIAN_POINT('Ctrl Pts',(14.8377974988368,0.630645044771057,3.83824960712979));
#13279=CARTESIAN_POINT('Ctrl Pts',(14.8614116149867,0.631851559871185,4.15697121131127));
#13280=CARTESIAN_POINT('Ctrl Pts',(14.8850257311365,0.481630465478622,4.4380735902585));
#13281=CARTESIAN_POINT('Ctrl Pts',(14.9061502929076,0.243989509668873,4.59562135563586));
#13282=CARTESIAN_POINT('Ctrl Pts',(14.9194034826287,0.0704409072858971,
4.62491684623921));
#13283=CARTESIAN_POINT('Ctrl Pts',(14.9247853002999,-1.38824472118368E-5,
4.62497559137666));
#13284=CARTESIAN_POINT('Origin',(11.8752146997001,0.,4.));
#13285=CARTESIAN_POINT('',(14.3247853002999,1.51969053300144E-5,4.6249871875462));
#13286=CARTESIAN_POINT('',(14.4252146997001,6.78316748347314E-6,4.62495403506715));
#13287=CARTESIAN_POINT('',(11.8752146997001,-1.68747709936658E-14,4.625));
#13288=CARTESIAN_POINT('Ctrl Pts',(14.4252146997001,6.78316748347826E-6,
4.62495403506715));
#13289=CARTESIAN_POINT('Ctrl Pts',(14.4297447157347,-0.0593027126443913,
4.62493103170719));
#13290=CARTESIAN_POINT('Ctrl Pts',(14.4421461038192,-0.221686029527806,
4.60198961095629));
#13291=CARTESIAN_POINT('Ctrl Pts',(14.4624188639536,-0.457506203155893,
4.46321101183598));
#13292=CARTESIAN_POINT('Ctrl Pts',(14.4860329801035,-0.622549707754089,
4.19054718257559));
#13293=CARTESIAN_POINT('Ctrl Pts',(14.5096470962533,-0.63839484111024,3.87221739454711));
#13294=CARTESIAN_POINT('Ctrl Pts',(14.5332612124032,-0.501244206711231,
3.58451159745434));
#13295=CARTESIAN_POINT('Ctrl Pts',(14.5568753285531,-0.243966908844842,
3.39638048838484));
#13296=CARTESIAN_POINT('Ctrl Pts',(14.5804894447029,0.0717787570654544,
3.35291099727801));
#13297=CARTESIAN_POINT('Ctrl Pts',(14.6041035608528,0.370322144162233,3.46452089026927));
#13298=CARTESIAN_POINT('Ctrl Pts',(14.6277176770027,0.580115251486915,3.70446207957941));
#13299=CARTESIAN_POINT('Ctrl Pts',(14.6513317931525,0.650879700384091,4.0152309888134));
#13300=CARTESIAN_POINT('Ctrl Pts',(14.6749459093024,0.565656298155129,4.32234968564526));
#13301=CARTESIAN_POINT('Ctrl Pts',(14.6985600254523,0.344869426209941,4.55221503612336));
#13302=CARTESIAN_POINT('Ctrl Pts',(14.7153162889182,0.129554394067723,4.62141618582314));
#13303=CARTESIAN_POINT('Ctrl Pts',(14.7242011803341,0.0132765736394338,
4.62504369367533));
#13304=CARTESIAN_POINT('Ctrl Pts',(14.7252146997001,1.17863019662174E-5,
4.62503218402409));
#13305=CARTESIAN_POINT('Ctrl Pts',(14.3247853002999,1.51969053300109E-5,
4.6249871875462));
#13306=CARTESIAN_POINT('Ctrl Pts',(14.3304905534298,-0.0746697890657793,
4.62491698721088));
#13307=CARTESIAN_POINT('Ctrl Pts',(14.3440671786096,-0.252453835406249,
4.59302599116618));
#13308=CARTESIAN_POINT('Ctrl Pts',(14.3655151758395,-0.490432948250941,
4.42819608115853));
#13309=CARTESIAN_POINT('Ctrl Pts',(14.3891292919893,-0.634910852255616,
4.14409916841427));
#13310=CARTESIAN_POINT('Ctrl Pts',(14.4127434081392,-0.627227950688033,
3.82546788683648));
#13311=CARTESIAN_POINT('Ctrl Pts',(14.4363575242891,-0.469225504392149,
3.54866444115539));
#13312=CARTESIAN_POINT('Ctrl Pts',(14.4599716404389,-0.198769899531221,
3.38002670405092));
#13313=CARTESIAN_POINT('Ctrl Pts',(14.4835857565888,0.11932229545683,3.35996988316441));
#13314=CARTESIAN_POINT('Ctrl Pts',(14.5071998727387,0.408818071695872,3.49330073524378));
#13315=CARTESIAN_POINT('Ctrl Pts',(14.5308139888885,0.600337751131954,3.74806559342675));
#13316=CARTESIAN_POINT('Ctrl Pts',(14.5544281050384,0.647982309355475,4.06320828594604));
#13317=CARTESIAN_POINT('Ctrl Pts',(14.5780422211883,0.540333396317157,4.36320267272319));
#13318=CARTESIAN_POINT('Ctrl Pts',(14.6014946196088,0.304813865567294,4.57469465218781));
#13319=CARTESIAN_POINT('Ctrl Pts',(14.6170756459793,0.100891269655612,4.62503197968527));
#13320=CARTESIAN_POINT('Ctrl Pts',(14.6247853002999,-2.16459804049194E-6,
4.62505212776347));
#13321=CARTESIAN_POINT('Origin',(11.8752146997001,0.,4.));
#13322=CARTESIAN_POINT('',(14.0247853002999,-6.3966029390794E-6,4.62495348172753));
#13323=CARTESIAN_POINT('',(14.1252146997001,-1.50974863142078E-5,4.62498583382255));
#13324=CARTESIAN_POINT('',(11.8752146997001,-1.68747709936658E-14,4.625));
#13325=CARTESIAN_POINT('Ctrl Pts',(14.1252146997001,-1.50974863141889E-5,
4.62498583382255));
#13326=CARTESIAN_POINT('Ctrl Pts',(14.1274168790852,-0.0288430498503269,
4.62501265364587));
#13327=CARTESIAN_POINT('Ctrl Pts',(14.1374904305203,-0.160695812902997,
4.61605202430223));
#13328=CARTESIAN_POINT('Ctrl Pts',(14.1554353540053,-0.385112282251534,
4.52494275637564));
#13329=CARTESIAN_POINT('Ctrl Pts',(14.1790494701552,-0.588131968915973,
4.27924389796604));
#13330=CARTESIAN_POINT('Ctrl Pts',(14.2026635863051,-0.65020173504413,3.96662229549764));
#13331=CARTESIAN_POINT('Ctrl Pts',(14.2262777024549,-0.556446129094758,
3.66199989226673));
#13332=CARTESIAN_POINT('Ctrl Pts',(14.2498918186048,-0.329334334698108,
3.43838156778717));
#13333=CARTESIAN_POINT('Ctrl Pts',(14.2735059347547,-0.0232952743833569,
3.34935901020328));
#13334=CARTESIAN_POINT('Ctrl Pts',(14.2971200509045,0.28832666060365,3.41626709515619));
#13335=CARTESIAN_POINT('Ctrl Pts',(14.3207341670544,0.530849104237583,3.62307083431711));
#13336=CARTESIAN_POINT('Ctrl Pts',(14.3443482832043,0.646149864620809,3.92020827196535));
#13337=CARTESIAN_POINT('Ctrl Pts',(14.3679623993541,0.606596311879891,4.2364683526943));
#13338=CARTESIAN_POINT('Ctrl Pts',(14.391576515504,0.42166773027486,4.49605714656388));
#13339=CARTESIAN_POINT('Ctrl Pts',(14.4106606156193,0.190545343529355,4.60977018898031));
#13340=CARTESIAN_POINT('Ctrl Pts',(14.4218733436847,0.0437536792250838,
4.62497100242767));
#13341=CARTESIAN_POINT('Ctrl Pts',(14.4252146997001,6.78316748347826E-6,
4.62495403506715));
#13342=CARTESIAN_POINT('Ctrl Pts',(14.0247853002999,-6.39660293913491E-6,
4.62495348172753));
#13343=CARTESIAN_POINT('Ctrl Pts',(14.0281627167804,-0.0442255271350925,
4.62496963662755));
#13344=CARTESIAN_POINT('Ctrl Pts',(14.0394115053108,-0.191490205391595,
4.6095527480466));
#13345=CARTESIAN_POINT('Ctrl Pts',(14.0585316658912,-0.422790583021024,
4.49510047824495));
#13346=CARTESIAN_POINT('Ctrl Pts',(14.0821457820411,-0.60713052675338,4.23509335195577));
#13347=CARTESIAN_POINT('Ctrl Pts',(14.1057598981909,-0.645967413308333,
3.91874446730605));
#13348=CARTESIAN_POINT('Ctrl Pts',(14.1293740143408,-0.529993712466286,
3.62186903671368));
#13349=CARTESIAN_POINT('Ctrl Pts',(14.1529881304907,-0.287003328966194,
3.41561532377041));
#13350=CARTESIAN_POINT('Ctrl Pts',(14.1766022466405,0.0247694002478971,
3.34941346658496));
#13351=CARTESIAN_POINT('Ctrl Pts',(14.2002163627904,0.330605970264406,3.43912920108534));
#13352=CARTESIAN_POINT('Ctrl Pts',(14.2238304789403,0.557210518047066,3.66326152695696));
#13353=CARTESIAN_POINT('Ctrl Pts',(14.2474445950901,0.650275686248857,3.96809557204375));
#13354=CARTESIAN_POINT('Ctrl Pts',(14.27105871124,0.587497759452106,4.28057573538778));
#13355=CARTESIAN_POINT('Ctrl Pts',(14.2946728273899,0.383921904832036,4.52581397056352));
#13356=CARTESIAN_POINT('Ctrl Pts',(14.3125816904098,0.159750963363977,4.61623247111552));
#13357=CARTESIAN_POINT('Ctrl Pts',(14.3226191813798,0.0283709170587055,
4.62501384057475));
#13358=CARTESIAN_POINT('Ctrl Pts',(14.3247853002999,1.51969053300109E-5,
4.6249871875462));
#13359=CARTESIAN_POINT('Origin',(11.8752146997001,0.,4.));
#13360=CARTESIAN_POINT('',(13.7247853002999,-1.20831421157597E-5,4.62503091248755));
#13361=CARTESIAN_POINT('',(13.8252146997001,1.68461488569462E-6,4.62505238998457));
#13362=CARTESIAN_POINT('',(11.8752146997001,-1.68747709936658E-14,4.625));
#13363=CARTESIAN_POINT('Ctrl Pts',(13.8252146997001,1.68461488569581E-6,
4.62505238998457));
#13364=CARTESIAN_POINT('Ctrl Pts',(13.8329604144858,-0.101363538932993,
4.62503644193381));
#13365=CARTESIAN_POINT('Ctrl Pts',(13.8485775013214,-0.305753798836605,
4.57432856173903));
#13366=CARTESIAN_POINT('Ctrl Pts',(13.8720659602069,-0.541154937947787,
4.36197748624323));
#13367=CARTESIAN_POINT('Ctrl Pts',(13.8956800763568,-0.648123865072376,
4.06173996222779));
#13368=CARTESIAN_POINT('Ctrl Pts',(13.9192941925067,-0.599765396122921,
3.74670602647169));
#13369=CARTESIAN_POINT('Ctrl Pts',(13.9429083086565,-0.407668974822819,
3.49237575473668));
#13370=CARTESIAN_POINT('Ctrl Pts',(13.9665224248064,-0.117871845784803,
3.35970116712309));
#13371=CARTESIAN_POINT('Ctrl Pts',(13.9901365409563,0.200174091641329,3.38047865214521));
#13372=CARTESIAN_POINT('Ctrl Pts',(14.0137506571061,0.470246914526057,3.54972874087838));
#13373=CARTESIAN_POINT('Ctrl Pts',(14.037364773256,0.627621790796785,3.82688947135059));
#13374=CARTESIAN_POINT('Ctrl Pts',(14.0609788894059,0.634582735815489,4.14553734509456));
#13375=CARTESIAN_POINT('Ctrl Pts',(14.0845930055557,0.489461510650943,4.42930618095194));
#13376=CARTESIAN_POINT('Ctrl Pts',(14.1060049423205,0.251510284961593,4.59332024860173));
#13377=CARTESIAN_POINT('Ctrl Pts',(14.1195455070353,0.074198300926532,4.62491679006221));
#13378=CARTESIAN_POINT('Ctrl Pts',(14.1252146997001,-1.50974863141889E-5,
4.62498583382255));
#13379=CARTESIAN_POINT('Ctrl Pts',(13.7247853002999,-1.20831421156938E-5,
4.62503091248755));
#13380=CARTESIAN_POINT('Ctrl Pts',(13.7258348801309,-0.013748904810447,
4.62504304225186));
#13381=CARTESIAN_POINT('Ctrl Pts',(13.734755832012,-0.130498998332177,4.62127102305724));
#13382=CARTESIAN_POINT('Ctrl Pts',(13.7515481559429,-0.346119716157775,
4.55143222859795));
#13383=CARTESIAN_POINT('Ctrl Pts',(13.7751622720928,-0.566385203513325,
4.32106722332061));
#13384=CARTESIAN_POINT('Ctrl Pts',(13.7987763882427,-0.650912534047929,
4.01375622291695));
#13385=CARTESIAN_POINT('Ctrl Pts',(13.8223905043925,-0.57944414457563,3.70314844792952));
#13386=CARTESIAN_POINT('Ctrl Pts',(13.8460046205424,-0.369107932149097,
3.46368321387984));
#13387=CARTESIAN_POINT('Ctrl Pts',(13.8696187366923,-0.0703124342978696,
3.35275003110641));
#13388=CARTESIAN_POINT('Ctrl Pts',(13.8932328528421,0.245333927901481,3.3969348091043));
#13389=CARTESIAN_POINT('Ctrl Pts',(13.916846968992,0.502184306426786,3.58564835824111));
#13390=CARTESIAN_POINT('Ctrl Pts',(13.9404610851419,0.638682720042094,3.87366416276737));
#13391=CARTESIAN_POINT('Ctrl Pts',(13.9640752012917,0.62211637371287,4.19195723015293));
#13392=CARTESIAN_POINT('Ctrl Pts',(13.9876893174416,0.456455507660852,4.46424641105313));
#13393=CARTESIAN_POINT('Ctrl Pts',(14.007926017111,0.220741531225703,4.60224444133776));
#13394=CARTESIAN_POINT('Ctrl Pts',(14.0202913447304,0.058831122868106,4.62493198618401));
#13395=CARTESIAN_POINT('Ctrl Pts',(14.0247853002999,-6.39660293913491E-6,
4.62495348172753));
#13396=CARTESIAN_POINT('Origin',(11.8752146997001,0.,4.));
#13397=CARTESIAN_POINT('',(13.4247853002999,1.36962628664028E-5,4.62502243215823));
#13398=CARTESIAN_POINT('',(13.5252146997001,1.40828270379035E-5,4.62497680637469));
#13399=CARTESIAN_POINT('',(11.8752146997001,-1.68747709936658E-14,4.625));
#13400=CARTESIAN_POINT('Ctrl Pts',(13.5252146997001,1.4082827037902E-5,
4.62497680637469));
#13401=CARTESIAN_POINT('Ctrl Pts',(13.5306325778363,-0.0709123884867814,
4.62491668074428));
#13402=CARTESIAN_POINT('Ctrl Pts',(13.5439218280225,-0.244933372371362,
4.59533688876844));
#13403=CARTESIAN_POINT('Ctrl Pts',(13.5650824502587,-0.482621788093898,
4.43698120905743));
#13404=CARTESIAN_POINT('Ctrl Pts',(13.5886965664085,-0.632205603168059,
4.15553919999523));
#13405=CARTESIAN_POINT('Ctrl Pts',(13.6123106825584,-0.630276944445953,
3.83682113889318));
#13406=CARTESIAN_POINT('Ctrl Pts',(13.6359247987083,-0.477298028416376,
3.55721002779864));
#13407=CARTESIAN_POINT('Ctrl Pts',(13.6595389148582,-0.209931317243796,
3.38371661595291));
#13408=CARTESIAN_POINT('Ctrl Pts',(13.683153031008,0.107746895509167,3.35791980725116));
#13409=CARTESIAN_POINT('Ctrl Pts',(13.7067671471579,0.399602814690774,3.48600198647908));
#13410=CARTESIAN_POINT('Ctrl Pts',(13.7303812633077,0.59569113756138,3.73726736776131));
#13411=CARTESIAN_POINT('Ctrl Pts',(13.7539953794576,0.649017932507905,4.05149845333026));
#13412=CARTESIAN_POINT('Ctrl Pts',(13.7776094956075,0.546803061895555,4.35338757606046));
#13413=CARTESIAN_POINT('Ctrl Pts',(13.8012236117573,0.313543031018869,4.57058490613733));
#13414=CARTESIAN_POINT('Ctrl Pts',(13.8170920131216,0.106300066848774,4.6246481407235));
#13415=CARTESIAN_POINT('Ctrl Pts',(13.8250890424358,0.00164611344283092,
4.62505264870678));
#13416=CARTESIAN_POINT('Ctrl Pts',(13.8252146997001,1.68461488569581E-6,
4.62505238998457));
#13417=CARTESIAN_POINT('Ctrl Pts',(13.4247853002999,1.36962628664097E-5,
4.62502243215823));
#13418=CARTESIAN_POINT('Ctrl Pts',(13.4313784155315,-0.086279884022628,
4.62493973056585));
#13419=CARTESIAN_POINT('Ctrl Pts',(13.445842902813,-0.275670893367246,4.58538934244717));
#13420=CARTESIAN_POINT('Ctrl Pts',(13.4681787621445,-0.513544980480383,
4.40018484937968));
#13421=CARTESIAN_POINT('Ctrl Pts',(13.4917928782944,-0.64195771209056,4.10847422061066));
#13422=CARTESIAN_POINT('Ctrl Pts',(13.5154069944443,-0.616520809113462,
3.79076698974655));
#13423=CARTESIAN_POINT('Ctrl Pts',(13.5390211105941,-0.443330402422436,
3.52320390633144));
#13424=CARTESIAN_POINT('Ctrl Pts',(13.562635226744,-0.163892778617988,3.36990832590288));
#13425=CARTESIAN_POINT('Ctrl Pts',(13.5862493428939,0.154822890495328,3.36761860145296));
#13426=CARTESIAN_POINT('Ctrl Pts',(13.6098634590437,0.43643417612693,3.51688348138565));
#13427=CARTESIAN_POINT('Ctrl Pts',(13.6334775751936,0.613450973283793,3.78193059814177));
#13428=CARTESIAN_POINT('Ctrl Pts',(13.6570916913435,0.643449974253473,4.09923956510808));
#13429=CARTESIAN_POINT('Ctrl Pts',(13.6807058074933,0.519241709620395,4.39276507945606));
#13430=CARTESIAN_POINT('Ctrl Pts',(13.7032703438121,0.281645253009076,4.58329909926801));
#13431=CARTESIAN_POINT('Ctrl Pts',(13.717963508081,0.0892710189108511,4.62495207452848));
#13432=CARTESIAN_POINT('Ctrl Pts',(13.7247853002999,-1.20831421156938E-5,
4.62503091248755));
#13433=CARTESIAN_POINT('Origin',(11.8752146997001,0.,4.));
#13434=CARTESIAN_POINT('',(13.1247853002999,3.84888821539087E-6,4.62495078081483));
#13435=CARTESIAN_POINT('',(13.2252146997001,-9.32440196476731E-6,4.62495874418382));
#13436=CARTESIAN_POINT('',(11.8752146997001,-1.68747709936658E-14,4.625));
#13437=CARTESIAN_POINT('Ctrl Pts',(13.2252146997001,-9.32440196474427E-6,
4.62495874418382));
#13438=CARTESIAN_POINT('Ctrl Pts',(13.2283047411869,-0.040464997295585,
4.62498052751194));
#13439=CARTESIAN_POINT('Ctrl Pts',(13.2392661547237,-0.18396024524725,4.61125364372682));
#13440=CARTESIAN_POINT('Ctrl Pts',(13.2580989403104,-0.413782468289504,
4.50265339583901));
#13441=CARTESIAN_POINT('Ctrl Pts',(13.2817130564603,-0.602786876612853,
4.24601696851145));
#13442=CARTESIAN_POINT('Ctrl Pts',(13.3053271726101,-0.647329213752593,
3.9304208620728));
#13443=CARTESIAN_POINT('Ctrl Pts',(13.32894128876,-0.536734598538914,3.6314998804023));
#13444=CARTESIAN_POINT('Ctrl Pts',(13.3525554049099,-0.297507800394296,
3.42089251764738));
#13445=CARTESIAN_POINT('Ctrl Pts',(13.3761695210598,0.0130188131672444,
3.34907229440132));
#13446=CARTESIAN_POINT('Ctrl Pts',(13.3997836372096,0.320425377524893,3.43325142712992));
#13447=CARTESIAN_POINT('Ctrl Pts',(13.4233977533595,0.551039769569266,3.65325580067535));
#13448=CARTESIAN_POINT('Ctrl Pts',(13.4470118695093,0.649593644862141,3.95635983539258));
#13449=CARTESIAN_POINT('Ctrl Pts',(13.4706259856592,0.592467881122722,4.26992253935193));
#13450=CARTESIAN_POINT('Ctrl Pts',(13.4942401018091,0.393353065302923,4.5187964277335));
#13451=CARTESIAN_POINT('Ctrl Pts',(13.5124363398227,0.1672808180195,4.61476328251587));
#13452=CARTESIAN_POINT('Ctrl Pts',(13.5227612057864,0.0321332374692893,
4.62500403435298));
#13453=CARTESIAN_POINT('Ctrl Pts',(13.5252146997001,1.4082827037902E-5,
4.62497680637469));
#13454=CARTESIAN_POINT('Ctrl Pts',(13.1247853002999,3.84888821536311E-6,
4.62495078081483));
#13455=CARTESIAN_POINT('Ctrl Pts',(13.1290505788821,-0.0558403875021823,
4.6249385719914));
#13456=CARTESIAN_POINT('Ctrl Pts',(13.1411872295142,-0.214751600407627,
4.60383286368317));
#13457=CARTESIAN_POINT('Ctrl Pts',(13.1611952521963,-0.449738236712957,
4.47075670902068));
#13458=CARTESIAN_POINT('Ctrl Pts',(13.1848093683461,-0.619294173608025,
4.2008758003961));
#13459=CARTESIAN_POINT('Ctrl Pts',(13.208423484496,-0.64043195068177,3.88285360784221));
#13460=CARTESIAN_POINT('Ctrl Pts',(13.2320376006459,-0.508085752511173,
3.59290636366459));
#13461=CARTESIAN_POINT('Ctrl Pts',(13.2556517167957,-0.253973266794505,
3.40052194335125));
#13462=CARTESIAN_POINT('Ctrl Pts',(13.2792658329456,0.0610056803032868,
3.3518066124833));
#13463=CARTESIAN_POINT('Ctrl Pts',(13.3028799490955,0.361364191435218,3.45843533922715));
#13464=CARTESIAN_POINT('Ctrl Pts',(13.3264940652453,0.575119258511334,3.69485380694));
#13465=CARTESIAN_POINT('Ctrl Pts',(13.3501081813952,0.65104299168552,4.00440268404554));
#13466=CARTESIAN_POINT('Ctrl Pts',(13.3737222975451,0.570939739771795,4.31289642727099));
#13467=CARTESIAN_POINT('Ctrl Pts',(13.3973364136949,0.354006804717113,4.54640236352309));
#13468=CARTESIAN_POINT('Ctrl Pts',(13.4143574146132,0.136489422610972,4.62032507485564));
#13469=CARTESIAN_POINT('Ctrl Pts',(13.4235070434815,0.0167440814458925,
4.62503846613771));
#13470=CARTESIAN_POINT('Ctrl Pts',(13.4247853002999,1.36962628664097E-5,
4.62502243215823));
#13471=CARTESIAN_POINT('Origin',(11.8752146997001,0.,4.));
#13472=CARTESIAN_POINT('',(12.8247853002999,-1.55438223423121E-5,4.62499607812274));
#13473=CARTESIAN_POINT('',(12.9252146997001,-9.4222586321007E-6,4.62504029123831));
#13474=CARTESIAN_POINT('',(11.8752146997001,-1.68747709936658E-14,4.625));
#13475=CARTESIAN_POINT('Ctrl Pts',(12.9252146997001,-9.42225863212465E-6,
4.62504029123832));
#13476=CARTESIAN_POINT('Ctrl Pts',(12.9259769045375,-0.00998466834883174,
4.6250476064301));
#13477=CARTESIAN_POINT('Ctrl Pts',(12.9346104814248,-0.122971475467856,
4.62239759066569));
#13478=CARTESIAN_POINT('Ctrl Pts',(12.9511154303622,-0.336107011072318,
4.55759164674784));
#13479=CARTESIAN_POINT('Ctrl Pts',(12.974729546512,-0.56049590900091,4.33124115596169));
#13480=CARTESIAN_POINT('Ctrl Pts',(12.9983436626619,-0.650558060547343,
4.02550641626558));
#13481=CARTESIAN_POINT('Ctrl Pts',(13.0219577788117,-0.584709444123524,
3.71365888635357));
#13482=CARTESIAN_POINT('Ctrl Pts',(13.0455718949616,-0.378731139057797,
3.47043499764384));
#13483=CARTESIAN_POINT('Ctrl Pts',(13.0691860111115,-0.0819872800401352,
3.35412504823007));
#13484=CARTESIAN_POINT('Ctrl Pts',(13.0928001272613,0.234405401379786,3.39260352716186));
#13485=CARTESIAN_POINT('Ctrl Pts',(13.1164142434112,0.494621196584012,3.57664879910166));
#13486=CARTESIAN_POINT('Ctrl Pts',(13.1400283595611,0.636297578801308,3.86215313342763));
#13487=CARTESIAN_POINT('Ctrl Pts',(13.1636424757109,0.625480816776257,4.18069342892634));
#13488=CARTESIAN_POINT('Ctrl Pts',(13.1872565918608,0.464763222827219,4.45592928631477));
#13489=CARTESIAN_POINT('Ctrl Pts',(13.2077806665239,0.228267895462889,4.60018049807294));
#13490=CARTESIAN_POINT('Ctrl Pts',(13.220433369137,0.0625891701764018,4.62492503806923));
#13491=CARTESIAN_POINT('Ctrl Pts',(13.2252146997001,-9.32440196474427E-6,
4.62495874418382));
#13492=CARTESIAN_POINT('Ctrl Pts',(12.8247853002999,-1.55438223423052E-5,
4.62499607812274));
#13493=CARTESIAN_POINT('Ctrl Pts',(12.8267227422326,-0.0253767156259869,
4.62502109614712));
#13494=CARTESIAN_POINT('Ctrl Pts',(12.8365315562153,-0.153759343851268,
4.61735081595804));
#13495=CARTESIAN_POINT('Ctrl Pts',(12.854211742248,-0.376327535803878,4.5312757721487));
#13496=CARTESIAN_POINT('Ctrl Pts',(12.8778258583979,-0.583405888470749,
4.28898776831928));
#13497=CARTESIAN_POINT('Ctrl Pts',(12.9014399745477,-0.650666957548692,
3.97744183415536));
#13498=CARTESIAN_POINT('Ctrl Pts',(12.9250540906976,-0.561991161265395,
3.67130212143154));
#13499=CARTESIAN_POINT('Ctrl Pts',(12.9486682068475,-0.338630270727757,
3.44393714350224));
#13500=CARTESIAN_POINT('Ctrl Pts',(12.9722823229973,-0.0341142786054444,
3.34983650006563));
#13501=CARTESIAN_POINT('Ctrl Pts',(12.9958964391472,0.278577437919422,3.41155206540036));
#13502=CARTESIAN_POINT('Ctrl Pts',(13.0195105552971,0.524506132150044,3.61429327464512));
#13503=CARTESIAN_POINT('Ctrl Pts',(13.0431246714469,0.644733280558021,3.90947178565704));
#13504=CARTESIAN_POINT('Ctrl Pts',(13.0667387875968,0.61044561006836,4.22634601343335));
#13505=CARTESIAN_POINT('Ctrl Pts',(13.0903529037467,0.429860399609997,4.4889748434194));
#13506=CARTESIAN_POINT('Ctrl Pts',(13.1097017413144,0.197481915229314,4.60814700801091));
#13507=CARTESIAN_POINT('Ctrl Pts',(13.1211792068321,0.0472175377905832,
4.6249611028038));
#13508=CARTESIAN_POINT('Ctrl Pts',(13.1247853002999,3.84888821536311E-6,
4.62495078081483));
#13509=CARTESIAN_POINT('Origin',(11.8752146997001,0.,4.));
#13510=CARTESIAN_POINT('',(12.5247853002999,3.80998376854277E-6,4.62503871776264));
#13511=CARTESIAN_POINT('',(12.6252146997001,1.49489494596481E-5,4.6250110476872));
#13512=CARTESIAN_POINT('',(11.8752146997001,-1.68747709936658E-14,4.625));
#13513=CARTESIAN_POINT('',(12.5,0.310062960217711,4.54266560670548));
#13514=CARTESIAN_POINT('Ctrl Pts',(12.5,0.310062960217722,4.54266560670548));
#13515=CARTESIAN_POINT('Ctrl Pts',(12.50787137205,0.220600394030941,4.59378185169648));
#13516=CARTESIAN_POINT('Ctrl Pts',(12.5161331388166,0.113220056708515,4.6237347594226));
#13517=CARTESIAN_POINT('Ctrl Pts',(12.5243949055832,0.00511234815255113,
4.6250406321328));
#13518=CARTESIAN_POINT('Ctrl Pts',(12.5247853002999,3.80998376856706E-6,
4.62503871776264));
#13519=CARTESIAN_POINT('',(12.5,0.310062960217774,3.45733439329455));
#13520=CARTESIAN_POINT('Origin',(12.5,0.,4.));
#13521=CARTESIAN_POINT('Ctrl Pts',(12.5,0.310093463203755,3.45730861053195));
#13522=CARTESIAN_POINT('Ctrl Pts',(12.5008157411716,0.319367492808711,3.46259780682489));
#13523=CARTESIAN_POINT('Ctrl Pts',(12.5095028543931,0.416666480413896,3.52147574364868));
#13524=CARTESIAN_POINT('Ctrl Pts',(12.5260613396645,0.569511032758309,3.68451895614546));
#13525=CARTESIAN_POINT('Ctrl Pts',(12.5496754558144,0.651018771792273,3.99264764559437));
#13526=CARTESIAN_POINT('Ctrl Pts',(12.5732895719643,0.576495013506714,4.3025367374363));
#13527=CARTESIAN_POINT('Ctrl Pts',(12.5969036881141,0.363815091701307,4.53992168461618));
#13528=CARTESIAN_POINT('Ctrl Pts',(12.6142120640261,0.144017971622128,4.61907377583531));
#13529=CARTESIAN_POINT('Ctrl Pts',(12.6236490678881,0.0205077016108913,
4.62503160004571));
#13530=CARTESIAN_POINT('Ctrl Pts',(12.6252146997001,1.49489494596471E-5,
4.6250110476872));
#13531=CARTESIAN_POINT('Origin',(11.8752146997001,0.,4.));
#13532=CARTESIAN_POINT('Ctrl Pts',(12.6252146997001,1.49489494596471E-5,
4.6250110476872));
#13533=CARTESIAN_POINT('Ctrl Pts',(12.631520439938,-0.0825216819810338,
4.62492827098767));
#13534=CARTESIAN_POINT('Ctrl Pts',(12.6456975522259,-0.268159494659544,
4.5879440580038));
#13535=CARTESIAN_POINT('Ctrl Pts',(12.6677460365637,-0.506235857616531,
4.40939182910775));
#13536=CARTESIAN_POINT('Ctrl Pts',(12.6913601527136,-0.639894509617229,
4.12004729681268));
#13537=CARTESIAN_POINT('Ctrl Pts',(12.7149742688635,-0.620198095551099,
3.8019325752266));
#13538=CARTESIAN_POINT('Ctrl Pts',(12.7385883850133,-0.451866840211785,
3.53128609963859));
#13539=CARTESIAN_POINT('Ctrl Pts',(12.7622025011632,-0.17524257447904,3.37297016902465));
#13540=CARTESIAN_POINT('Ctrl Pts',(12.7858166173131,0.143379805101228,3.36492630429559));
#13541=CARTESIAN_POINT('Ctrl Pts',(12.809430733463,0.42764021116234,3.50908227080648));
#13542=CARTESIAN_POINT('Ctrl Pts',(12.8330448496128,0.609413666055986,3.77089008898231));
#13543=CARTESIAN_POINT('Ctrl Pts',(12.8566589657627,0.645136892431096,4.08760569204938));
#13544=CARTESIAN_POINT('Ctrl Pts',(12.8802730819125,0.526248572038732,4.38332598125533));
#13545=CARTESIAN_POINT('Ctrl Pts',(12.903124993225,0.289149347937084,4.5805996458561));
#13546=CARTESIAN_POINT('Ctrl Pts',(12.9181055324875,0.0930307802739178,
4.62497206165088));
#13547=CARTESIAN_POINT('Ctrl Pts',(12.9252146997001,-9.42225863212465E-6,
4.62504029123832));
#13548=CARTESIAN_POINT('Ctrl Pts',(12.5247853002999,3.80998376856706E-6,
4.62503871776264));
#13549=CARTESIAN_POINT('Ctrl Pts',(12.5322662776332,-0.0978890574527522,
4.62500203345524));
#13550=CARTESIAN_POINT('Ctrl Pts',(12.5476186270164,-0.298862923743373,
4.57698368148067));
#13551=CARTESIAN_POINT('Ctrl Pts',(12.5708423484496,-0.535054221536356,
4.37092866956447));
#13552=CARTESIAN_POINT('Ctrl Pts',(12.5944564645995,-0.647009713430093,
4.07251155115386));
#13553=CARTESIAN_POINT('Ctrl Pts',(12.6180705807493,-0.603894380709874,
3.75671714932517));
#13554=CARTESIAN_POINT('Ctrl Pts',(12.6416846968992,-0.416056506175611,
3.49922677321964));
#13555=CARTESIAN_POINT('Ctrl Pts',(12.6652988130491,-0.128505496873939,
3.36175035317655));
#13556=CARTESIAN_POINT('Ctrl Pts',(12.6889129291989,0.189841674427298,3.37723482234205));
#13557=CARTESIAN_POINT('Ctrl Pts',(12.7125270453488,0.462692468193658,3.54196933898577));
#13558=CARTESIAN_POINT('Ctrl Pts',(12.7361411614987,0.624655556881011,3.81647407445394));
#13559=CARTESIAN_POINT('Ctrl Pts',(12.7597552776485,0.636915702199809,4.13496208375113));
#13560=CARTESIAN_POINT('Ctrl Pts',(12.7833693937984,0.496534514683115,4.42110548633398));
#13561=CARTESIAN_POINT('Ctrl Pts',(12.8050460680155,0.258436396781676,4.5911312751119));
#13562=CARTESIAN_POINT('Ctrl Pts',(12.8188513701827,0.0776597756952025,
4.62491945378327));
#13563=CARTESIAN_POINT('Ctrl Pts',(12.8247853002999,-1.55438223423052E-5,
4.62499607812274));
#13564=CARTESIAN_POINT('Ctrl Pts',(12.5,-0.186196943290592,3.58169363627332));
#13565=CARTESIAN_POINT('Ctrl Pts',(12.50787137205,-0.117235947257613,3.55099764935784));
#13566=CARTESIAN_POINT('Ctrl Pts',(12.5236141161499,0.0360970477778841,
3.52440632583991));
#13567=CARTESIAN_POINT('Ctrl Pts',(12.5472282322997,0.257537368848111,3.59853698535937));
#13568=CARTESIAN_POINT('Ctrl Pts',(12.5708423484496,0.417223782598737,3.76887858727216));
#13569=CARTESIAN_POINT('Ctrl Pts',(12.5944564645995,0.476936352215019,3.99461366516243));
#13570=CARTESIAN_POINT('Ctrl Pts',(12.6180705807493,0.422340246895018,4.22163841384584));
#13571=CARTESIAN_POINT('Ctrl Pts',(12.6416846968992,0.266530936180377,4.39554662614981));
#13572=CARTESIAN_POINT('Ctrl Pts',(12.6652988130491,0.0468439715927196,
4.47465904879863));
#13573=CARTESIAN_POINT('Ctrl Pts',(12.6889129291989,-0.184068700558194,
4.44001626345752));
#13574=CARTESIAN_POINT('Ctrl Pts',(12.7125270453488,-0.37086838928987,4.29992045400434));
#13575=CARTESIAN_POINT('Ctrl Pts',(12.7361411614987,-0.468786717745582,
4.08794664964497));
#13576=CARTESIAN_POINT('Ctrl Pts',(12.7597552776485,-0.454357124800734,
3.85489580461101));
#13577=CARTESIAN_POINT('Ctrl Pts',(12.7833693937984,-0.331037647139153,
3.65662019659523));
#13578=CARTESIAN_POINT('Ctrl Pts',(12.8069835099483,-0.128382710063344,
3.54063794582746));
#13579=CARTESIAN_POINT('Ctrl Pts',(12.8305976260981,0.10504004521716,3.53474501052695));
#13580=CARTESIAN_POINT('Ctrl Pts',(12.854211742248,0.31328921869753,3.64035367159283));
#13581=CARTESIAN_POINT('Ctrl Pts',(12.8778258583979,0.446456451752615,3.83215407918844));
#13582=CARTESIAN_POINT('Ctrl Pts',(12.9014399745477,0.47262728739502,4.06417992999538));
#13583=CARTESIAN_POINT('Ctrl Pts',(12.9250540906976,0.385529703875575,4.28082461386765));
#13584=CARTESIAN_POINT('Ctrl Pts',(12.9486682068475,0.206037242841946,4.43016772408018));
#13585=CARTESIAN_POINT('Ctrl Pts',(12.9722823229973,-0.0228334776507366,
4.47641814468844));
#13586=CARTESIAN_POINT('Ctrl Pts',(12.9958964391472,-0.24623199631158,4.40849164040747));
#13587=CARTESIAN_POINT('Ctrl Pts',(13.0195105552971,-0.410619302934066,
4.24266727085754));
#13588=CARTESIAN_POINT('Ctrl Pts',(13.0431246714469,-0.476598835156983,
4.01868600055616));
#13589=CARTESIAN_POINT('Ctrl Pts',(13.0667387875968,-0.428358138764893,
3.79022650014263));
#13590=CARTESIAN_POINT('Ctrl Pts',(13.0903529037467,-0.277458432473742,
3.61204067927388));
#13591=CARTESIAN_POINT('Ctrl Pts',(13.1139670198965,-0.060063881357403,
3.52683201033335));
#13592=CARTESIAN_POINT('Ctrl Pts',(13.1375811360464,0.171725397050831,3.55502134399878));
#13593=CARTESIAN_POINT('Ctrl Pts',(13.1611952521963,0.362359488617447,3.68985291022187));
#13594=CARTESIAN_POINT('Ctrl Pts',(13.1848093683461,0.466151606229838,3.89901338554908));
#13595=CARTESIAN_POINT('Ctrl Pts',(13.208423484496,0.458227246370285,4.13237600603144));
#13596=CARTESIAN_POINT('Ctrl Pts',(13.2320376006459,0.34048553704322,4.3340137951542));
#13597=CARTESIAN_POINT('Ctrl Pts',(13.2556517167957,0.141144098528766,4.45560285308526));
#13598=CARTESIAN_POINT('Ctrl Pts',(13.2792658329456,-0.0920235057499227,
4.46800351566886));
#13599=CARTESIAN_POINT('Ctrl Pts',(13.3028799490955,-0.30313703626889,4.36824387779166));
#13600=CARTESIAN_POINT('Ctrl Pts',(13.3264940652453,-0.441601665806575,
4.18023203113149));
#13601=CARTESIAN_POINT('Ctrl Pts',(13.3501081813952,-0.47423338199515,3.94902632355453));
#13602=CARTESIAN_POINT('Ctrl Pts',(13.3737222975451,-0.393211766889608,
3.73003681238273));
#13603=CARTESIAN_POINT('Ctrl Pts',(13.3973364136949,-0.217954214568861,
3.57574585842847));
#13604=CARTESIAN_POINT('Ctrl Pts',(13.4209505298448,0.00953758252632317,
3.52313036287841));
#13605=CARTESIAN_POINT('Ctrl Pts',(13.4445646459947,0.234743631574736,3.58479999551538));
#13606=CARTESIAN_POINT('Ctrl Pts',(13.4681787621445,0.403691735186444,3.74597519957476));
#13607=CARTESIAN_POINT('Ctrl Pts',(13.4917928782944,0.475892304226004,3.96802921540861));
#13608=CARTESIAN_POINT('Ctrl Pts',(13.5154069944443,0.434041969710506,4.19774525232923));
#13609=CARTESIAN_POINT('Ctrl Pts',(13.5390211105941,0.288170455640921,4.38007026295756));
#13610=CARTESIAN_POINT('Ctrl Pts',(13.562635226744,0.0732368858249759,4.47130878927046));
#13611=CARTESIAN_POINT('Ctrl Pts',(13.5862493428939,-0.159248413505658,
4.44959488329479));
#13612=CARTESIAN_POINT('Ctrl Pts',(13.6098634590437,-0.353568721957589,
4.32013243375547));
#13613=CARTESIAN_POINT('Ctrl Pts',(13.6334775751936,-0.46315382488092,4.1139480179165));
#13614=CARTESIAN_POINT('Ctrl Pts',(13.6570916913435,-0.461740889501104,
3.88045516635315));
#13615=CARTESIAN_POINT('Ctrl Pts',(13.6807058074933,-0.349668535617837,
3.67561206636528));
#13616=CARTESIAN_POINT('Ctrl Pts',(13.7043199236432,-0.153795683012805,
3.5485107928471));
#13617=CARTESIAN_POINT('Ctrl Pts',(13.7279340397931,0.0789353756500159,
3.5296120507922));
#13618=CARTESIAN_POINT('Ctrl Pts',(13.7515481559429,0.292749022042461,3.62344505529457));
#13619=CARTESIAN_POINT('Ctrl Pts',(13.7751622720928,0.436403327377467,3.80752207362193));
#13620=CARTESIAN_POINT('Ctrl Pts',(13.7987763882427,0.475470537355291,4.03772776690975));
#13621=CARTESIAN_POINT('Ctrl Pts',(13.8223905043925,0.400587923144683,4.25889173822189));
#13622=CARTESIAN_POINT('Ctrl Pts',(13.8460046205424,0.229701624524423,4.41801050223621));
#13623=CARTESIAN_POINT('Ctrl Pts',(13.8696187366923,0.00376573255618155,
4.47695013947711));
#13624=CARTESIAN_POINT('Ctrl Pts',(13.8932328528421,-0.223072643433687,
4.42158535558109));
#13625=CARTESIAN_POINT('Ctrl Pts',(13.916846968992,-0.396450107540549,4.26518470642179));
#13626=CARTESIAN_POINT('Ctrl Pts',(13.9404610851419,-0.474815543552022,
4.04523069632808));
#13627=CARTESIAN_POINT('Ctrl Pts',(13.9640752012917,-0.439388129199652,
3.81443683499316));
#13628=CARTESIAN_POINT('Ctrl Pts',(13.9876893174416,-0.298658290955197,
3.62811447792009));
#13629=CARTESIAN_POINT('Ctrl Pts',(14.0113034335915,-0.0863529142219465,
3.53091707503438));
#13630=CARTESIAN_POINT('Ctrl Pts',(14.0349175497413,0.146647539536438,3.54613866056158));
#13631=CARTESIAN_POINT('Ctrl Pts',(14.0585316658912,0.344502889581789,3.6701312755675));
#13632=CARTESIAN_POINT('Ctrl Pts',(14.0821457820411,0.459795723937725,3.87317922671144));
#13633=CARTESIAN_POINT('Ctrl Pts',(14.1057598981909,0.464895312258427,4.10662065901627));
#13634=CARTESIAN_POINT('Ctrl Pts',(14.1293740143408,0.358579502702881,4.31450970816539));
#13635=CARTESIAN_POINT('Ctrl Pts',(14.1529881304907,0.166327619131383,4.44702431634421));
#13636=CARTESIAN_POINT('Ctrl Pts',(14.1766022466405,-0.0657858362277661,
4.47240643522367));
#13637=CARTESIAN_POINT('Ctrl Pts',(14.2002163627904,-0.282133257977474,
4.38457306332079));
#13638=CARTESIAN_POINT('Ctrl Pts',(14.2238304789403,-0.430865480427841,
4.20457407964992));
#13639=CARTESIAN_POINT('Ctrl Pts',(14.2474445950901,-0.476337791093329,
3.97554749368157));
#13640=CARTESIAN_POINT('Ctrl Pts',(14.27105871124,-0.407652434174819,3.75238112107461));
#13641=CARTESIAN_POINT('Ctrl Pts',(14.2946728273899,-0.241270333599833,
3.58855833656088));
#13642=CARTESIAN_POINT('Ctrl Pts',(14.3182869435397,-0.0170661180132474,
3.52334041087493));
#13643=CARTESIAN_POINT('Ctrl Pts',(14.3419010596896,0.211228111558234,3.57235727391142));
#13644=CARTESIAN_POINT('Ctrl Pts',(14.3655151758395,0.388900053764453,3.72386169322071));
#13645=CARTESIAN_POINT('Ctrl Pts',(14.3891292919893,0.473369390821204,3.94154458004181));
#13646=CARTESIAN_POINT('Ctrl Pts',(14.4127434081392,0.444392458083208,4.17323671518384));
#13647=CARTESIAN_POINT('Ctrl Pts',(14.4363575242891,0.308913779199362,4.3634114655727));
#13648=CARTESIAN_POINT('Ctrl Pts',(14.4599716404389,0.0994017626770733,
4.46649212840691));
#13649=CARTESIAN_POINT('Ctrl Pts',(14.4835857565888,-0.133932578240045,
4.45777470525894));
#13650=CARTESIAN_POINT('Ctrl Pts',(14.5071998727387,-0.335169044432007,
4.33934838727104));
#13651=CARTESIAN_POINT('Ctrl Pts',(14.5308139888885,-0.456079915900645,
4.13959486595487));
#13652=CARTESIAN_POINT('Ctrl Pts',(14.5544281050384,-0.467688060597361,
3.90638646324521));
#13653=CARTESIAN_POINT('Ctrl Pts',(14.5780422211883,-0.367211505836647,
3.69561319629505));
#13654=CARTESIAN_POINT('Ctrl Pts',(14.6016563373381,-0.178730157419731,
3.55778834579073));
#13655=CARTESIAN_POINT('Ctrl Pts',(14.625270453488,0.0525851174261518,3.52594259660587));
#13656=CARTESIAN_POINT('Ctrl Pts',(14.6488845696379,0.271298002813252,3.60770800421126));
#13657=CARTESIAN_POINT('Ctrl Pts',(14.6724986857877,0.424992433239313,3.78348891949988));
#13658=CARTESIAN_POINT('Ctrl Pts',(14.6961128019376,0.476834468501385,4.01115822240469));
#13659=CARTESIAN_POINT('Ctrl Pts',(14.7197269180875,0.414399804028447,4.23615337970372));
#13660=CARTESIAN_POINT('Ctrl Pts',(14.7433410342373,0.252651341641402,4.40455273546398));
#13661=CARTESIAN_POINT('Ctrl Pts',(14.7669551503872,0.0303532266559796,
4.47599821226155));
#13662=CARTESIAN_POINT('Ctrl Pts',(14.7905692665371,-0.199219250862459,
4.43336740322118));
#13663=CARTESIAN_POINT('Ctrl Pts',(14.8141833826869,-0.381047447081096,
4.28687708064914));
#13664=CARTESIAN_POINT('Ctrl Pts',(14.8377974988368,-0.471554972144783,
4.07163466550741));
#13665=CARTESIAN_POINT('Ctrl Pts',(14.8614116149867,-0.449051060899263,
3.83922451083896));
#13666=CARTESIAN_POINT('Ctrl Pts',(14.8850257311365,-0.318928946727196,
3.64534530693059));
#13667=CARTESIAN_POINT('Ctrl Pts',(14.9086398472864,-0.112373269271187,
3.53646160000302));
#13668=CARTESIAN_POINT('Ctrl Pts',(14.9322539634362,0.121113399391719,3.5386680312482));
#13669=CARTESIAN_POINT('Ctrl Pts',(14.9558680795861,0.325574495333277,3.65143602219853));
#13670=CARTESIAN_POINT('Ctrl Pts',(14.979482195736,0.452009190454857,3.84773949289016));
#13671=CARTESIAN_POINT('Ctrl Pts',(15.0030963118858,0.470117180575255,4.08053390545391));
#13672=CARTESIAN_POINT('Ctrl Pts',(15.0267104280357,0.375557372208547,4.29402641177155));
#13673=CARTESIAN_POINT('Ctrl Pts',(15.0503245441856,0.190994688421392,4.43705643304037));
#13674=CARTESIAN_POINT('Ctrl Pts',(15.0739386603355,-0.0393454023191647,
4.47533644032795));
#13675=CARTESIAN_POINT('Ctrl Pts',(15.0975527764853,-0.260245916509526,
4.39971253597763));
#13676=CARTESIAN_POINT('Ctrl Pts',(15.1211668926352,-0.418792603204267,
4.22826540530875));
#13677=CARTESIAN_POINT('Ctrl Pts',(15.1369096367351,-0.457530945318996,
4.07754232577813));
#13678=CARTESIAN_POINT('Ctrl Pts',(15.1447810087851,-0.457870370902723,
4.00205890126089));
#13679=CARTESIAN_POINT('Ctrl Pts',(12.4850729970717,-0.208850989443975,
3.53079950502365));
#13680=CARTESIAN_POINT('Ctrl Pts',(12.4929443691216,-0.131499707516366,
3.49636882573344));
#13681=CARTESIAN_POINT('Ctrl Pts',(12.5086871132215,0.0404888716816997,
3.46654221242176));
#13682=CARTESIAN_POINT('Ctrl Pts',(12.5323012293714,0.288871199237585,3.54969213591223));
#13683=CARTESIAN_POINT('Ctrl Pts',(12.5559153455212,0.467986199318594,3.74075871022993));
#13684=CARTESIAN_POINT('Ctrl Pts',(12.5795294616711,0.534963825407437,3.99395832530641));
#13685=CARTESIAN_POINT('Ctrl Pts',(12.603143577821,0.473725169098917,4.24860452170932));
#13686=CARTESIAN_POINT('Ctrl Pts',(12.6267576939708,0.298958988020687,4.4436716456386));
#13687=CARTESIAN_POINT('Ctrl Pts',(12.6503718101207,0.0525433427838623,
4.53240944903922));
#13688=CARTESIAN_POINT('Ctrl Pts',(12.6739859262706,-0.206463809544117,
4.49355177571912));
#13689=CARTESIAN_POINT('Ctrl Pts',(12.6976000424205,-0.41599087873209,4.33641091237214));
#13690=CARTESIAN_POINT('Ctrl Pts',(12.7212141585703,-0.525822648369464,
4.09864686536754));
#13691=CARTESIAN_POINT('Ctrl Pts',(12.7448282747202,-0.509637448384189,
3.8372413948162));
#13692=CARTESIAN_POINT('Ctrl Pts',(12.76844239087,-0.37131404483003,3.61484216427635));
#13693=CARTESIAN_POINT('Ctrl Pts',(12.7920565070199,-0.144002664868576,
3.48474868689319));
#13694=CARTESIAN_POINT('Ctrl Pts',(12.8156706231698,0.117819965178516,3.47813877511649));
#13695=CARTESIAN_POINT('Ctrl Pts',(12.8392847393197,0.351406216185799,3.59659653799738));
#13696=CARTESIAN_POINT('Ctrl Pts',(12.8628988554695,0.500775523187073,3.81173274911973));
#13697=CARTESIAN_POINT('Ctrl Pts',(12.8865129716194,0.530130489073712,4.07198851734671));
#13698=CARTESIAN_POINT('Ctrl Pts',(12.9101270877692,0.432435993263294,4.31499173633021));
#13699=CARTESIAN_POINT('Ctrl Pts',(12.9337412039191,0.231105201134755,4.48250499290311));
#13700=CARTESIAN_POINT('Ctrl Pts',(12.957355320069,-0.0256115611541523,
4.53438256906268));
#13701=CARTESIAN_POINT('Ctrl Pts',(12.9809694362189,-0.276190334565159,
4.45819164252092));
#13702=CARTESIAN_POINT('Ctrl Pts',(13.0045835523687,-0.460578171623014,
4.27219189922559));
#13703=CARTESIAN_POINT('Ctrl Pts',(13.0281976685186,-0.534585243620437,
4.0209594724593));
#13704=CARTESIAN_POINT('Ctrl Pts',(13.0518117846684,-0.480475240551103,
3.76470396221295));
#13705=CARTESIAN_POINT('Ctrl Pts',(13.0754259008183,-0.311216001335094,
3.5648387853972));
#13706=CARTESIAN_POINT('Ctrl Pts',(13.0990400169682,-0.0673716809183137,
3.46926302296559));
#13707=CARTESIAN_POINT('Ctrl Pts',(13.122654133118,0.19261873182715,3.50088207171981));
#13708=CARTESIAN_POINT('Ctrl Pts',(13.1462682492679,0.406446724606302,3.65211820651514));
#13709=CARTESIAN_POINT('Ctrl Pts',(13.1698823654178,0.522866930420328,3.88672663484193));
#13710=CARTESIAN_POINT('Ctrl Pts',(13.1934964815676,0.513978436505609,4.14848181366307));
#13711=CARTESIAN_POINT('Ctrl Pts',(13.2171105977175,0.381911432304553,4.37465229220773));
#13712=CARTESIAN_POINT('Ctrl Pts',(13.2407247138674,0.158316694737061,4.51103474084347));
#13713=CARTESIAN_POINT('Ctrl Pts',(13.2643388300172,-0.103219740820234,
4.52494415635039));
#13714=CARTESIAN_POINT('Ctrl Pts',(13.2879529461671,-0.340018846942428,
4.41304705047411));
#13715=CARTESIAN_POINT('Ctrl Pts',(13.311567062317,-0.495330069408668,4.20216034359148));
#13716=CARTESIAN_POINT('Ctrl Pts',(13.3351811784669,-0.531931992580964,
3.94282450306062));
#13717=CARTESIAN_POINT('Ctrl Pts',(13.3587952946167,-0.44105271077271,3.69719116838925));
#13718=CARTESIAN_POINT('Ctrl Pts',(13.3824094107666,-0.244472076510672,
3.5241280781681));
#13719=CARTESIAN_POINT('Ctrl Pts',(13.4060235269164,0.0106979927399635,
3.46511100671938));
#13720=CARTESIAN_POINT('Ctrl Pts',(13.4296376430663,0.263304213558122,3.53428380605355));
#13721=CARTESIAN_POINT('Ctrl Pts',(13.4532517592162,0.452807746647384,3.71506873327496));
#13722=CARTESIAN_POINT('Ctrl Pts',(13.476865875366,0.533792751104717,3.96413942206993));
#13723=CARTESIAN_POINT('Ctrl Pts',(13.5004799915159,0.486850606847911,4.22180434800346));
#13724=CARTESIAN_POINT('Ctrl Pts',(13.5240941076658,0.323231325528255,4.42631231788287));
#13725=CARTESIAN_POINT('Ctrl Pts',(13.5477082238157,0.0821474069231642,
4.52865157307741));
#13726=CARTESIAN_POINT('Ctrl Pts',(13.5713223399655,-0.178623709606947,
4.50429579866153));
#13727=CARTESIAN_POINT('Ctrl Pts',(13.5949364561154,-0.396586410669692,
4.35908202552279));
#13728=CARTESIAN_POINT('Ctrl Pts',(13.6185505722652,-0.519504417643299,
4.12781174527607));
#13729=CARTESIAN_POINT('Ctrl Pts',(13.6421646884151,-0.517919574482721,
3.86591049053316));
#13730=CARTESIAN_POINT('Ctrl Pts',(13.665778804565,-0.392211699884016,3.6361447201764));
#13731=CARTESIAN_POINT('Ctrl Pts',(13.6893929207148,-0.172507561089802,
3.49357940054904));
#13732=CARTESIAN_POINT('Ctrl Pts',(13.7130070368647,0.0885392156030666,
3.47238130294519));
#13733=CARTESIAN_POINT('Ctrl Pts',(13.7366211530146,0.328366952925232,3.57763069902274));
#13734=CARTESIAN_POINT('Ctrl Pts',(13.7602352691644,0.489499264105438,3.78410383833506));
#13735=CARTESIAN_POINT('Ctrl Pts',(13.7838493853143,0.533319669072828,4.04231799571659));
#13736=CARTESIAN_POINT('Ctrl Pts',(13.8074635014642,0.449326302728307,4.29039035083475));
#13737=CARTESIAN_POINT('Ctrl Pts',(13.831077617614,0.257648760022572,4.46886863686992));
#13738=CARTESIAN_POINT('Ctrl Pts',(13.8546917337639,0.00422389839726028,
4.53497929012603));
#13739=CARTESIAN_POINT('Ctrl Pts',(13.8783058499138,-0.25021324988294,4.47287843233165));
#13740=CARTESIAN_POINT('Ctrl Pts',(13.9019199660636,-0.444685051009628,
4.29744896636227));
#13741=CARTESIAN_POINT('Ctrl Pts',(13.9255340822135,-0.532584984058807,
4.05073378496132));
#13742=CARTESIAN_POINT('Ctrl Pts',(13.9491481983634,-0.492847218174075,
3.79185989881933));
#13743=CARTESIAN_POINT('Ctrl Pts',(13.9727623145132,-0.334995185577738,
3.58286823685896));
#13744=CARTESIAN_POINT('Ctrl Pts',(13.9963764306631,-0.0968592247428986,
3.47384510573062));
#13745=CARTESIAN_POINT('Ctrl Pts',(14.019990546813,0.164489723571401,3.49091865775613));
#13746=CARTESIAN_POINT('Ctrl Pts',(14.0436046629628,0.386417564563212,3.62999709733779));
#13747=CARTESIAN_POINT('Ctrl Pts',(14.0672187791127,0.515737746224078,3.85774930825782));
#13748=CARTESIAN_POINT('Ctrl Pts',(14.0908328952626,0.521457786777448,4.11959288770904));
#13749=CARTESIAN_POINT('Ctrl Pts',(14.1144470114124,0.402206838685568,4.35277519909424));
#13750=CARTESIAN_POINT('Ctrl Pts',(14.1380611275623,0.186564221804844,4.50141247822903));
#13751=CARTESIAN_POINT('Ctrl Pts',(14.1616752437122,-0.0737898095680628,
4.52988276645436));
#13752=CARTESIAN_POINT('Ctrl Pts',(14.185289359862,-0.316459599402161,4.43136296100575));
#13753=CARTESIAN_POINT('Ctrl Pts',(14.2089034760119,-0.483287643257218,
4.22946401908862));
#13754=CARTESIAN_POINT('Ctrl Pts',(14.2325175921618,-0.53429243907693,3.97257242762026));
#13755=CARTESIAN_POINT('Ctrl Pts',(14.2561317083116,-0.457250332481466,
3.72225404480531));
#13756=CARTESIAN_POINT('Ctrl Pts',(14.2797458244615,-0.270625000632592,
3.53849941363631));
#13757=CARTESIAN_POINT('Ctrl Pts',(14.3033599406114,-0.0191425034699505,
3.46534661065105));
#13758=CARTESIAN_POINT('Ctrl Pts',(14.3269740567612,0.236927627906706,3.52032721432634));
#13759=CARTESIAN_POINT('Ctrl Pts',(14.3505881729111,0.436216403922163,3.69026474025285));
#13760=CARTESIAN_POINT('Ctrl Pts',(14.374202289061,0.530962882087739,3.93443247734966));
#13761=CARTESIAN_POINT('Ctrl Pts',(14.3978164052108,0.498460409348769,4.19431392768733));
#13762=CARTESIAN_POINT('Ctrl Pts',(14.4214305213607,0.346498429557861,4.40762669256976));
#13763=CARTESIAN_POINT('Ctrl Pts',(14.4450446375106,0.111495689030631,4.52324888295055));
#13764=CARTESIAN_POINT('Ctrl Pts',(14.4686587536604,-0.150227769531968,
4.51347083601981));
#13765=CARTESIAN_POINT('Ctrl Pts',(14.4922728698103,-0.375948097339969,
4.38063592879268));
#13766=CARTESIAN_POINT('Ctrl Pts',(14.5158869859602,-0.51156984651846,4.15657897149511));
#13767=CARTESIAN_POINT('Ctrl Pts',(14.53950110211,-0.52459032076832,3.89499677367918));
#13768=CARTESIAN_POINT('Ctrl Pts',(14.5631152182599,-0.411889072794842,
3.65857933001481));
#13769=CARTESIAN_POINT('Ctrl Pts',(14.5867293344098,-0.200475741228102,
3.50398572665543));
#13770=CARTESIAN_POINT('Ctrl Pts',(14.6103434505596,0.0589829973059192,
3.46826539682992));
#13771=CARTESIAN_POINT('Ctrl Pts',(14.6339575667095,0.304306049929579,3.5599789662306));
#13772=CARTESIAN_POINT('Ctrl Pts',(14.6575716828594,0.476700039321847,3.75714663952638));
#13773=CARTESIAN_POINT('Ctrl Pts',(14.6811857990092,0.53484954579562,4.0125158112076));
#13774=CARTESIAN_POINT('Ctrl Pts',(14.7047999151591,0.464818635404008,4.26488548168423));
#13775=CARTESIAN_POINT('Ctrl Pts',(14.728414031309,0.283390703164248,4.45377350235044));
#13776=CARTESIAN_POINT('Ctrl Pts',(14.7520281474588,0.0340462163765225,
4.5339115446661));
#13777=CARTESIAN_POINT('Ctrl Pts',(14.7756422636087,-0.223457683695575,
4.48609396779546));
#13778=CARTESIAN_POINT('Ctrl Pts',(14.7992563797586,-0.427408393186059,
4.32178058932398));
#13779=CARTESIAN_POINT('Ctrl Pts',(14.8228704959084,-0.528927708313459,
4.08035024907128));
#13780=CARTESIAN_POINT('Ctrl Pts',(14.8464846120583,-0.503685810960444,
3.81966341983811));
#13781=CARTESIAN_POINT('Ctrl Pts',(14.8700987282082,-0.357732113691821,
3.6021954912391));
#13782=CARTESIAN_POINT('Ctrl Pts',(14.893712844358,-0.126045401495737,3.48006421709321));
#13783=CARTESIAN_POINT('Ctrl Pts',(14.9173269605079,0.13584891809103,3.48253909847714));
#13784=CARTESIAN_POINT('Ctrl Pts',(14.9409410766578,0.365186207068703,3.60902724630258));
#13785=CARTESIAN_POINT('Ctrl Pts',(14.9645551928076,0.507003847624586,3.82921439524653));
#13786=CARTESIAN_POINT('Ctrl Pts',(14.9881693089575,0.52731498478211,4.0903322339271));
#13787=CARTESIAN_POINT('Ctrl Pts',(15.0117834251074,0.421250356706029,4.32979975898591));
#13788=CARTESIAN_POINT('Ctrl Pts',(15.0353975412572,0.214232462415332,4.49023183125449));
#13789=CARTESIAN_POINT('Ctrl Pts',(15.0590116574071,-0.0441324441701724,
4.53316925684615));
#13790=CARTESIAN_POINT('Ctrl Pts',(15.082625773557,-0.291909288096862,4.4483444097243));
#13791=CARTESIAN_POINT('Ctrl Pts',(15.1062398897068,-0.469745893811612,
4.25603780014884));
#13792=CARTESIAN_POINT('Ctrl Pts',(15.1219826338067,-0.513197418509596,
4.08697667736293));
#13793=CARTESIAN_POINT('Ctrl Pts',(15.1298540058567,-0.513578141027115,
4.0023094018511));
#13794=CARTESIAN_POINT('Ctrl Pts',(12.4701459941433,-0.231505035597357,
3.47990537377399));
#13795=CARTESIAN_POINT('Ctrl Pts',(12.4780173661933,-0.145763467775118,
3.44174000210903));
#13796=CARTESIAN_POINT('Ctrl Pts',(12.4937601102932,0.0448806955855158,
3.40867809900361));
#13797=CARTESIAN_POINT('Ctrl Pts',(12.517374226443,0.320205029627059,3.5008472864651));
#13798=CARTESIAN_POINT('Ctrl Pts',(12.5409883425929,0.518748616038451,3.71263883318769));
#13799=CARTESIAN_POINT('Ctrl Pts',(12.5646024587428,0.592991298599855,3.99330298545039));
#13800=CARTESIAN_POINT('Ctrl Pts',(12.5882165748926,0.525110091302815,4.27557062957281));
#13801=CARTESIAN_POINT('Ctrl Pts',(12.6118306910425,0.331387039860997,4.49179666512739));
#13802=CARTESIAN_POINT('Ctrl Pts',(12.6354448071924,0.0582427139750047,
4.5901598492798));
#13803=CARTESIAN_POINT('Ctrl Pts',(12.6590589233422,-0.22885891853004,4.54708728798072));
#13804=CARTESIAN_POINT('Ctrl Pts',(12.6826730394921,-0.461113368174311,
4.37290137073994));
#13805=CARTESIAN_POINT('Ctrl Pts',(12.706287155642,-0.582858578993347,4.10934708109011));
#13806=CARTESIAN_POINT('Ctrl Pts',(12.7299012717918,-0.564917771967644,
3.8195869850214));
#13807=CARTESIAN_POINT('Ctrl Pts',(12.7535153879417,-0.411590442520908,
3.57306413195747));
#13808=CARTESIAN_POINT('Ctrl Pts',(12.7771295040916,-0.159622619673808,
3.42885942795892));
#13809=CARTESIAN_POINT('Ctrl Pts',(12.8007436202414,0.130599885139872,3.42153253970604));
#13810=CARTESIAN_POINT('Ctrl Pts',(12.8243577363913,0.38952321367407,3.55283940440193));
#13811=CARTESIAN_POINT('Ctrl Pts',(12.8479718525412,0.555094594621529,3.79131141905102));
#13812=CARTESIAN_POINT('Ctrl Pts',(12.871585968691,0.587633690752404,4.07979710469805));
#13813=CARTESIAN_POINT('Ctrl Pts',(12.8952000848409,0.479342282651013,4.34915885879276));
#13814=CARTESIAN_POINT('Ctrl Pts',(12.9188142009908,0.256173159427565,4.53484226172604));
#13815=CARTESIAN_POINT('Ctrl Pts',(12.9424283171406,-0.0283896446575681,
4.59234699343691));
#13816=CARTESIAN_POINT('Ctrl Pts',(12.9660424332905,-0.306148672818738,
4.50789164463438));
#13817=CARTESIAN_POINT('Ctrl Pts',(12.9896565494404,-0.510537040311962,
4.30171652759364));
#13818=CARTESIAN_POINT('Ctrl Pts',(13.0132706655902,-0.59257165208389,4.02323294436244));
#13819=CARTESIAN_POINT('Ctrl Pts',(13.0368847817401,-0.532592342337314,
3.73918142428326));
#13820=CARTESIAN_POINT('Ctrl Pts',(13.06049889789,-0.344973570196446,3.51763689152052));
#13821=CARTESIAN_POINT('Ctrl Pts',(13.0841130140398,-0.0746794804792245,
3.41169403559782));
#13822=CARTESIAN_POINT('Ctrl Pts',(13.1077271301897,0.213512066603468,3.44674279944083));
#13823=CARTESIAN_POINT('Ctrl Pts',(13.1313412463396,0.450533960595157,3.6143835028084));
#13824=CARTESIAN_POINT('Ctrl Pts',(13.1549553624894,0.579582254610818,3.87443988413478));
#13825=CARTESIAN_POINT('Ctrl Pts',(13.1785694786393,0.569729626640933,4.1645876212947));
#13826=CARTESIAN_POINT('Ctrl Pts',(13.2021835947892,0.423337327565886,4.41529078926125));
#13827=CARTESIAN_POINT('Ctrl Pts',(13.225797710939,0.175489290945357,4.56646662860168));
#13828=CARTESIAN_POINT('Ctrl Pts',(13.2494118270889,-0.114415975890545,
4.58188479703192));
#13829=CARTESIAN_POINT('Ctrl Pts',(13.2730259432388,-0.376900657615966,
4.45785022315656));
#13830=CARTESIAN_POINT('Ctrl Pts',(13.2966400593886,-0.54905847301076,4.22408865605146));
#13831=CARTESIAN_POINT('Ctrl Pts',(13.3202541755385,-0.589630603166779,
3.93662268256671));
#13832=CARTESIAN_POINT('Ctrl Pts',(13.3438682916884,-0.488893654655812,
3.66434552439578));
#13833=CARTESIAN_POINT('Ctrl Pts',(13.3674824078382,-0.270989938452484,
3.47251029790774));
#13834=CARTESIAN_POINT('Ctrl Pts',(13.3910965239881,0.0118584029536041,
3.40709165056035));
#13835=CARTESIAN_POINT('Ctrl Pts',(13.414710640138,0.291864795541507,3.48376761659174));
#13836=CARTESIAN_POINT('Ctrl Pts',(13.4383247562878,0.501923758108325,3.68416226697515));
#13837=CARTESIAN_POINT('Ctrl Pts',(13.4619388724377,0.591693197983429,3.96024962873126));
#13838=CARTESIAN_POINT('Ctrl Pts',(13.4855529885876,0.539659243985316,4.2458634436777));
#13839=CARTESIAN_POINT('Ctrl Pts',(13.5091671047374,0.358292195415589,4.47255437280819));
#13840=CARTESIAN_POINT('Ctrl Pts',(13.5327812208873,0.0910579280213527,
4.58599435688436));
#13841=CARTESIAN_POINT('Ctrl Pts',(13.5563953370372,-0.197999005708236,
4.55899671402827));
#13842=CARTESIAN_POINT('Ctrl Pts',(13.580009453187,-0.439604099381795,4.39803161729011));
#13843=CARTESIAN_POINT('Ctrl Pts',(13.6036235693369,-0.575855010405679,
4.14167547263565));
#13844=CARTESIAN_POINT('Ctrl Pts',(13.6272376854868,-0.574098259464336,
3.85136581471317));
#13845=CARTESIAN_POINT('Ctrl Pts',(13.6508518016366,-0.434754864150196,
3.59667737398752));
#13846=CARTESIAN_POINT('Ctrl Pts',(13.6744659177865,-0.191219439166798,
3.43864800825098));
#13847=CARTESIAN_POINT('Ctrl Pts',(13.6980800339364,0.0981430555561168,
3.41515055509818));
#13848=CARTESIAN_POINT('Ctrl Pts',(13.7216941500862,0.363984883808003,3.53181634275091));
#13849=CARTESIAN_POINT('Ctrl Pts',(13.7453082662361,0.54259520083341,3.76068560304818));
#13850=CARTESIAN_POINT('Ctrl Pts',(13.768922382386,0.591168800790367,4.04690822452342));
#13851=CARTESIAN_POINT('Ctrl Pts',(13.7925364985358,0.498064682311931,4.32188896344761));
#13852=CARTESIAN_POINT('Ctrl Pts',(13.8161506146857,0.28559589552072,4.51972677150362));
#13853=CARTESIAN_POINT('Ctrl Pts',(13.8397647308356,0.00468206423833927,
4.59300844077494));
#13854=CARTESIAN_POINT('Ctrl Pts',(13.8633788469854,-0.277353856332193,
4.52417150908221));
#13855=CARTESIAN_POINT('Ctrl Pts',(13.8869929631353,-0.492919994478707,
4.32971322630275));
#13856=CARTESIAN_POINT('Ctrl Pts',(13.9106070792852,-0.590354424565592,
4.05623687359455));
#13857=CARTESIAN_POINT('Ctrl Pts',(13.934221195435,-0.546306307148498,3.76928296264551));
#13858=CARTESIAN_POINT('Ctrl Pts',(13.9578353115849,-0.371332080200278,
3.53762199579782));
#13859=CARTESIAN_POINT('Ctrl Pts',(13.9814494277348,-0.107365535263851,
3.41677313642685));
#13860=CARTESIAN_POINT('Ctrl Pts',(14.0050635438846,0.182331907606365,3.43569865495067));
#13861=CARTESIAN_POINT('Ctrl Pts',(14.0286776600345,0.428332239544634,3.58986291910809));
#13862=CARTESIAN_POINT('Ctrl Pts',(14.0522917761844,0.571679768510432,3.8423193898042));
#13863=CARTESIAN_POINT('Ctrl Pts',(14.0759058923342,0.578020261296468,4.1325651164018));
#13864=CARTESIAN_POINT('Ctrl Pts',(14.0995200084841,0.445834174668256,4.39104069002309));
#13865=CARTESIAN_POINT('Ctrl Pts',(14.123134124634,0.206800824478305,4.55580064011384));
#13866=CARTESIAN_POINT('Ctrl Pts',(14.1467482407838,-0.0817937829083601,
4.58735909768505));
#13867=CARTESIAN_POINT('Ctrl Pts',(14.1703623569337,-0.350785940826847,
4.4781528586907));
#13868=CARTESIAN_POINT('Ctrl Pts',(14.1939764730836,-0.535709806086595,
4.25435395852733));
#13869=CARTESIAN_POINT('Ctrl Pts',(14.2175905892334,-0.59224708706053,3.96959736155895));
#13870=CARTESIAN_POINT('Ctrl Pts',(14.2412047053833,-0.506848230788112,
3.69212696853602));
#13871=CARTESIAN_POINT('Ctrl Pts',(14.2648188215332,-0.29997966766535,3.48844049071174));
#13872=CARTESIAN_POINT('Ctrl Pts',(14.288432937683,-0.0212188889266537,
3.40735281042717));
#13873=CARTESIAN_POINT('Ctrl Pts',(14.3120470538329,0.262627144255178,3.46829715474127));
#13874=CARTESIAN_POINT('Ctrl Pts',(14.3356611699828,0.483532754079872,3.65666778728498));
#13875=CARTESIAN_POINT('Ctrl Pts',(14.3592752861326,0.588556373354274,3.9273203746575));
#13876=CARTESIAN_POINT('Ctrl Pts',(14.3828894022825,0.55252836061433,4.21539114019081));
#13877=CARTESIAN_POINT('Ctrl Pts',(14.4065035184324,0.384083079916361,4.45184191956682));
#13878=CARTESIAN_POINT('Ctrl Pts',(14.4301176345822,0.123589615384189,4.58000563749418));
#13879=CARTESIAN_POINT('Ctrl Pts',(14.4537317507321,-0.166522960823891,
4.56916696678068));
#13880=CARTESIAN_POINT('Ctrl Pts',(14.477345866882,-0.416727150247931,4.42192347031433));
#13881=CARTESIAN_POINT('Ctrl Pts',(14.5009599830318,-0.567059777136274,
4.17356307703535));
#13882=CARTESIAN_POINT('Ctrl Pts',(14.5245740991817,-0.58149258093928,3.88360708411314));
#13883=CARTESIAN_POINT('Ctrl Pts',(14.5481882153316,-0.456566639753037,
3.62154546373458));
#13884=CARTESIAN_POINT('Ctrl Pts',(14.5718023314814,-0.222221325036472,
3.45018310752014));
#13885=CARTESIAN_POINT('Ctrl Pts',(14.5954164476313,0.0653808771856868,
3.41058819705396));
#13886=CARTESIAN_POINT('Ctrl Pts',(14.6190305637812,0.337314097045906,3.51224992824993));
#13887=CARTESIAN_POINT('Ctrl Pts',(14.642644679931,0.528407645404381,3.73080435955289));
#13888=CARTESIAN_POINT('Ctrl Pts',(14.6662587960809,0.592864623089856,4.0138734000105));
#13889=CARTESIAN_POINT('Ctrl Pts',(14.6898729122308,0.515237466779568,4.29361758366474));
#13890=CARTESIAN_POINT('Ctrl Pts',(14.7134870283806,0.314130064687094,4.5029942692369));
#13891=CARTESIAN_POINT('Ctrl Pts',(14.7371011445305,0.0377392060970651,
4.59182487707066));
#13892=CARTESIAN_POINT('Ctrl Pts',(14.7607152606804,-0.24769611652869,4.53882053236973));
#13893=CARTESIAN_POINT('Ctrl Pts',(14.7843293768302,-0.47376933929102,4.35668409799883));
#13894=CARTESIAN_POINT('Ctrl Pts',(14.8079434929801,-0.586300444482135,
4.08906583263515));
#13895=CARTESIAN_POINT('Ctrl Pts',(14.83155760913,-0.558320561021625,3.80010232883727));
#13896=CARTESIAN_POINT('Ctrl Pts',(14.8551717252798,-0.396535280656446,
3.55904567554761));
#13897=CARTESIAN_POINT('Ctrl Pts',(14.8787858414297,-0.139717533720287,
3.42366683418339));
#13898=CARTESIAN_POINT('Ctrl Pts',(14.9023999575795,0.150584436790342,3.42641016570609));
#13899=CARTESIAN_POINT('Ctrl Pts',(14.9260140737294,0.404797918804129,3.56661847040663));
#13900=CARTESIAN_POINT('Ctrl Pts',(14.9496281898793,0.561998504794314,3.8106892976029));
#13901=CARTESIAN_POINT('Ctrl Pts',(14.9732423060292,0.584512788988964,4.10013056240029));
#13902=CARTESIAN_POINT('Ctrl Pts',(14.996856422179,0.466943341203511,4.36557310620026));
#13903=CARTESIAN_POINT('Ctrl Pts',(15.0204705383289,0.237470236409271,4.54340722946861));
#13904=CARTESIAN_POINT('Ctrl Pts',(15.0440846544788,-0.0489194860211801,
4.59100207336435));
#13905=CARTESIAN_POINT('Ctrl Pts',(15.0676987706286,-0.323572659684198,
4.49697628347096));
#13906=CARTESIAN_POINT('Ctrl Pts',(15.0913128867785,-0.520699184418956,
4.28381019498893));
#13907=CARTESIAN_POINT('Ctrl Pts',(15.1070556308784,-0.568863891700195,
4.09641102894772));
#13908=CARTESIAN_POINT('Ctrl Pts',(15.1149270029284,-0.569285911151507,
4.00255990244131));
#13909=CARTESIAN_POINT('Ctrl Pts',(12.455218991215,-0.25415908175074,3.42901124252432));
#13910=CARTESIAN_POINT('Ctrl Pts',(12.4630903632649,-0.16002722803387,3.38711117848463));
#13911=CARTESIAN_POINT('Ctrl Pts',(12.4788331073648,0.0492725194893315,
3.35081398558546));
#13912=CARTESIAN_POINT('Ctrl Pts',(12.5024472235147,0.351538860016532,3.45200243701797));
#13913=CARTESIAN_POINT('Ctrl Pts',(12.5260613396645,0.569511032758309,3.68451895614546));
#13914=CARTESIAN_POINT('Ctrl Pts',(12.5496754558144,0.651018771792273,3.99264764559437));
#13915=CARTESIAN_POINT('Ctrl Pts',(12.5732895719643,0.576495013506714,4.3025367374363));
#13916=CARTESIAN_POINT('Ctrl Pts',(12.5969036881141,0.363815091701307,4.53992168461618));
#13917=CARTESIAN_POINT('Ctrl Pts',(12.620517804264,0.0639420851661475,4.64791024952038));
#13918=CARTESIAN_POINT('Ctrl Pts',(12.6441319204139,-0.251254027515963,
4.60062280024232));
#13919=CARTESIAN_POINT('Ctrl Pts',(12.6677460365637,-0.506235857616531,
4.40939182910775));
#13920=CARTESIAN_POINT('Ctrl Pts',(12.6913601527136,-0.639894509617229,
4.12004729681268));
#13921=CARTESIAN_POINT('Ctrl Pts',(12.7149742688635,-0.620198095551099,
3.8019325752266));
#13922=CARTESIAN_POINT('Ctrl Pts',(12.7385883850133,-0.451866840211785,
3.53128609963859));
#13923=CARTESIAN_POINT('Ctrl Pts',(12.7622025011632,-0.17524257447904,3.37297016902465));
#13924=CARTESIAN_POINT('Ctrl Pts',(12.7858166173131,0.143379805101228,3.36492630429559));
#13925=CARTESIAN_POINT('Ctrl Pts',(12.809430733463,0.42764021116234,3.50908227080648));
#13926=CARTESIAN_POINT('Ctrl Pts',(12.8330448496128,0.609413666055986,3.77089008898231));
#13927=CARTESIAN_POINT('Ctrl Pts',(12.8566589657627,0.645136892431096,4.08760569204938));
#13928=CARTESIAN_POINT('Ctrl Pts',(12.8802730819125,0.526248572038732,4.38332598125533));
#13929=CARTESIAN_POINT('Ctrl Pts',(12.9038871980624,0.281241117720374,4.58717953054897));
#13930=CARTESIAN_POINT('Ctrl Pts',(12.9275013142123,-0.0311677281609838,
4.65031141781114));
#13931=CARTESIAN_POINT('Ctrl Pts',(12.9511154303622,-0.336107011072318,
4.55759164674784));
#13932=CARTESIAN_POINT('Ctrl Pts',(12.974729546512,-0.56049590900091,4.33124115596169));
#13933=CARTESIAN_POINT('Ctrl Pts',(12.9983436626619,-0.650558060547343,
4.02550641626558));
#13934=CARTESIAN_POINT('Ctrl Pts',(13.0219577788117,-0.584709444123524,
3.71365888635357));
#13935=CARTESIAN_POINT('Ctrl Pts',(13.0455718949616,-0.378731139057797,
3.47043499764384));
#13936=CARTESIAN_POINT('Ctrl Pts',(13.0691860111115,-0.0819872800401352,
3.35412504823007));
#13937=CARTESIAN_POINT('Ctrl Pts',(13.0928001272613,0.234405401379786,3.39260352716186));
#13938=CARTESIAN_POINT('Ctrl Pts',(13.1164142434112,0.494621196584012,3.57664879910166));
#13939=CARTESIAN_POINT('Ctrl Pts',(13.1400283595611,0.636297578801308,3.86215313342763));
#13940=CARTESIAN_POINT('Ctrl Pts',(13.1636424757109,0.625480816776257,4.18069342892634));
#13941=CARTESIAN_POINT('Ctrl Pts',(13.1872565918608,0.464763222827219,4.45592928631477));
#13942=CARTESIAN_POINT('Ctrl Pts',(13.2108707080107,0.192661887153653,4.62189851635989));
#13943=CARTESIAN_POINT('Ctrl Pts',(13.2344848241605,-0.125612210960856,
4.63882543771344));
#13944=CARTESIAN_POINT('Ctrl Pts',(13.2580989403104,-0.413782468289504,
4.50265339583901));
#13945=CARTESIAN_POINT('Ctrl Pts',(13.2817130564603,-0.602786876612853,
4.24601696851145));
#13946=CARTESIAN_POINT('Ctrl Pts',(13.3053271726101,-0.647329213752593,
3.9304208620728));
#13947=CARTESIAN_POINT('Ctrl Pts',(13.32894128876,-0.536734598538914,3.6314998804023));
#13948=CARTESIAN_POINT('Ctrl Pts',(13.3525554049099,-0.297507800394296,
3.42089251764738));
#13949=CARTESIAN_POINT('Ctrl Pts',(13.3761695210598,0.0130188131672444,
3.34907229440132));
#13950=CARTESIAN_POINT('Ctrl Pts',(13.3997836372096,0.320425377524893,3.43325142712992));
#13951=CARTESIAN_POINT('Ctrl Pts',(13.4233977533595,0.551039769569266,3.65325580067535));
#13952=CARTESIAN_POINT('Ctrl Pts',(13.4470118695093,0.649593644862141,3.95635983539258));
#13953=CARTESIAN_POINT('Ctrl Pts',(13.4706259856592,0.592467881122722,4.26992253935193));
#13954=CARTESIAN_POINT('Ctrl Pts',(13.4942401018091,0.393353065302923,4.5187964277335));
#13955=CARTESIAN_POINT('Ctrl Pts',(13.5178542179589,0.0999684491195412,
4.64333714069132));
#13956=CARTESIAN_POINT('Ctrl Pts',(13.5414683341088,-0.217374301809525,
4.61369762939502));
#13957=CARTESIAN_POINT('Ctrl Pts',(13.5650824502587,-0.482621788093898,
4.43698120905743));
#13958=CARTESIAN_POINT('Ctrl Pts',(13.5886965664085,-0.632205603168059,
4.15553919999523));
#13959=CARTESIAN_POINT('Ctrl Pts',(13.6123106825584,-0.630276944445953,
3.83682113889318));
#13960=CARTESIAN_POINT('Ctrl Pts',(13.6359247987083,-0.477298028416376,
3.55721002779864));
#13961=CARTESIAN_POINT('Ctrl Pts',(13.6595389148582,-0.209931317243796,
3.38371661595291));
#13962=CARTESIAN_POINT('Ctrl Pts',(13.683153031008,0.107746895509167,3.35791980725116));
#13963=CARTESIAN_POINT('Ctrl Pts',(13.7067671471579,0.399602814690774,3.48600198647908));
#13964=CARTESIAN_POINT('Ctrl Pts',(13.7303812633077,0.59569113756138,3.73726736776131));
#13965=CARTESIAN_POINT('Ctrl Pts',(13.7539953794576,0.649017932507905,4.05149845333026));
#13966=CARTESIAN_POINT('Ctrl Pts',(13.7776094956075,0.546803061895555,4.35338757606046));
#13967=CARTESIAN_POINT('Ctrl Pts',(13.8012236117573,0.313543031018869,4.57058490613733));
#13968=CARTESIAN_POINT('Ctrl Pts',(13.8248377279072,0.00514023007941788,
4.65103759142385));
#13969=CARTESIAN_POINT('Ctrl Pts',(13.8484518440571,-0.304494462781446,
4.57546458583277));
#13970=CARTESIAN_POINT('Ctrl Pts',(13.8720659602069,-0.541154937947787,
4.36197748624323));
#13971=CARTESIAN_POINT('Ctrl Pts',(13.8956800763568,-0.648123865072376,
4.06173996222779));
#13972=CARTESIAN_POINT('Ctrl Pts',(13.9192941925067,-0.599765396122921,
3.74670602647169));
#13973=CARTESIAN_POINT('Ctrl Pts',(13.9429083086565,-0.407668974822819,
3.49237575473668));
#13974=CARTESIAN_POINT('Ctrl Pts',(13.9665224248064,-0.117871845784803,
3.35970116712309));
#13975=CARTESIAN_POINT('Ctrl Pts',(13.9901365409563,0.200174091641329,3.38047865214521));
#13976=CARTESIAN_POINT('Ctrl Pts',(14.0137506571061,0.470246914526057,3.54972874087838));
#13977=CARTESIAN_POINT('Ctrl Pts',(14.037364773256,0.627621790796785,3.82688947135059));
#13978=CARTESIAN_POINT('Ctrl Pts',(14.0609788894059,0.634582735815489,4.14553734509456));
#13979=CARTESIAN_POINT('Ctrl Pts',(14.0845930055557,0.489461510650943,4.42930618095194));
#13980=CARTESIAN_POINT('Ctrl Pts',(14.1082071217056,0.227037427151766,4.61018880199865));
#13981=CARTESIAN_POINT('Ctrl Pts',(14.1318212378555,-0.0897977562486571,
4.64483542891575));
#13982=CARTESIAN_POINT('Ctrl Pts',(14.1554353540053,-0.385112282251534,
4.52494275637564));
#13983=CARTESIAN_POINT('Ctrl Pts',(14.1790494701552,-0.588131968915973,
4.27924389796604));
#13984=CARTESIAN_POINT('Ctrl Pts',(14.2026635863051,-0.65020173504413,3.96662229549764));
#13985=CARTESIAN_POINT('Ctrl Pts',(14.2262777024549,-0.556446129094758,
3.66199989226673));
#13986=CARTESIAN_POINT('Ctrl Pts',(14.2498918186048,-0.329334334698108,
3.43838156778717));
#13987=CARTESIAN_POINT('Ctrl Pts',(14.2735059347547,-0.0232952743833569,
3.34935901020328));
#13988=CARTESIAN_POINT('Ctrl Pts',(14.2971200509045,0.28832666060365,3.41626709515619));
#13989=CARTESIAN_POINT('Ctrl Pts',(14.3207341670544,0.530849104237583,3.62307083431711));
#13990=CARTESIAN_POINT('Ctrl Pts',(14.3443482832043,0.646149864620809,3.92020827196535));
#13991=CARTESIAN_POINT('Ctrl Pts',(14.3679623993541,0.606596311879891,4.2364683526943));
#13992=CARTESIAN_POINT('Ctrl Pts',(14.391576515504,0.42166773027486,4.49605714656388));
#13993=CARTESIAN_POINT('Ctrl Pts',(14.4151906316539,0.135683541737747,4.63676239203782));
#13994=CARTESIAN_POINT('Ctrl Pts',(14.4388047478037,-0.182818152115814,
4.62486309754155));
#13995=CARTESIAN_POINT('Ctrl Pts',(14.4624188639536,-0.457506203155893,
4.46321101183598));
#13996=CARTESIAN_POINT('Ctrl Pts',(14.4860329801035,-0.622549707754089,
4.19054718257559));
#13997=CARTESIAN_POINT('Ctrl Pts',(14.5096470962533,-0.63839484111024,3.87221739454711));
#13998=CARTESIAN_POINT('Ctrl Pts',(14.5332612124032,-0.501244206711231,
3.58451159745434));
#13999=CARTESIAN_POINT('Ctrl Pts',(14.5568753285531,-0.243966908844842,
3.39638048838484));
#14000=CARTESIAN_POINT('Ctrl Pts',(14.5804894447029,0.0717787570654544,
3.35291099727801));
#14001=CARTESIAN_POINT('Ctrl Pts',(14.6041035608528,0.370322144162233,3.46452089026927));
#14002=CARTESIAN_POINT('Ctrl Pts',(14.6277176770027,0.580115251486915,3.70446207957941));
#14003=CARTESIAN_POINT('Ctrl Pts',(14.6513317931525,0.650879700384091,4.0152309888134));
#14004=CARTESIAN_POINT('Ctrl Pts',(14.6749459093024,0.565656298155129,4.32234968564526));
#14005=CARTESIAN_POINT('Ctrl Pts',(14.6985600254523,0.344869426209941,4.55221503612336));
#14006=CARTESIAN_POINT('Ctrl Pts',(14.7221741416021,0.041432195817608,4.64973820947522));
#14007=CARTESIAN_POINT('Ctrl Pts',(14.745788257752,-0.271934549361806,4.59154709694401));
#14008=CARTESIAN_POINT('Ctrl Pts',(14.7694023739019,-0.520130285395982,
4.39158760667368));
#14009=CARTESIAN_POINT('Ctrl Pts',(14.7930164900517,-0.64367318065081,4.09778141619902));
#14010=CARTESIAN_POINT('Ctrl Pts',(14.8166306062016,-0.612955311082805,
3.78054123783642));
#14011=CARTESIAN_POINT('Ctrl Pts',(14.8402447223515,-0.435338447621071,
3.51589585985611));
#14012=CARTESIAN_POINT('Ctrl Pts',(14.8638588385013,-0.153389665944836,
3.36726945127358));
#14013=CARTESIAN_POINT('Ctrl Pts',(14.8874729546512,0.165319955489652,3.37028123293502));
#14014=CARTESIAN_POINT('Ctrl Pts',(14.9110870708011,0.444409630539555,3.52420969451069));
#14015=CARTESIAN_POINT('Ctrl Pts',(14.9347011869509,0.616993161964042,3.79216419995926));
#14016=CARTESIAN_POINT('Ctrl Pts',(14.9583153031008,0.641710593195818,4.10992889087348));
#14017=CARTESIAN_POINT('Ctrl Pts',(14.9819294192507,0.512636325700993,4.40134645341462));
#14018=CARTESIAN_POINT('Ctrl Pts',(15.0055435354005,0.260708010403211,4.59658262768273));
#14019=CARTESIAN_POINT('Ctrl Pts',(15.0291576515504,-0.0537065278721878,
4.64883488988255));
#14020=CARTESIAN_POINT('Ctrl Pts',(15.0527717677003,-0.355236031271534,
4.54560815721762));
#14021=CARTESIAN_POINT('Ctrl Pts',(15.0763858838501,-0.571652475026301,
4.31158258982903));
#14022=CARTESIAN_POINT('Ctrl Pts',(15.09212862795,-0.624530364890795,4.10584538053252));
#14023=CARTESIAN_POINT('Ctrl Pts',(15.1,-0.624993681275899,4.00281040303152));
#14024=CARTESIAN_POINT('Ctrl Pts',(15.1,-0.624993681275899,4.00281040303152));
#14025=CARTESIAN_POINT('Ctrl Pts',(15.1,-0.617358358083874,4.02914127082806));
#14026=CARTESIAN_POINT('Ctrl Pts',(15.1,-0.607931963506944,4.05484759228836));
#14027=CARTESIAN_POINT('Ctrl Pts',(15.1,-0.596773861259576,4.07974656001827));
#14028=CARTESIAN_POINT('Ctrl Pts',(15.1,-0.585871522029423,4.10407480030985));
#14029=CARTESIAN_POINT('Ctrl Pts',(15.1,-0.573314772633929,4.12763281365198));
#14030=CARTESIAN_POINT('Ctrl Pts',(15.1,-0.559143639302279,4.1502040881484));
#14031=CARTESIAN_POINT('Ctrl Pts',(15.1,-0.549626121151564,4.16536325076984));
#14032=CARTESIAN_POINT('Ctrl Pts',(15.1,-0.539380106047495,4.18007635520315));
#14033=CARTESIAN_POINT('Ctrl Pts',(15.1,-0.528417753985571,4.19426420824267));
#14034=CARTESIAN_POINT('Ctrl Pts',(15.1,-0.523814643226911,4.2002217124899));
#14035=CARTESIAN_POINT('Ctrl Pts',(15.1,-0.519084627089791,4.20608691507751));
#14036=CARTESIAN_POINT('Ctrl Pts',(15.1,-0.514239086396905,4.21184190560023));
#14037=CARTESIAN_POINT('Ctrl Pts',(15.1,-0.50085552272952,4.2277374035328));
#14038=CARTESIAN_POINT('Ctrl Pts',(15.1,-0.486572803760524,4.24281789068328));
#14039=CARTESIAN_POINT('Ctrl Pts',(15.1,-0.4714177983537,4.25697008589974));
#14040=CARTESIAN_POINT('Ctrl Pts',(15.1,-0.457151696655403,4.27029219637033));
#14041=CARTESIAN_POINT('Ctrl Pts',(15.1,-0.442112042545397,4.28279146400573));
#14042=CARTESIAN_POINT('Ctrl Pts',(15.1,-0.426369607892924,4.29437520287289));
#14043=CARTESIAN_POINT('Ctrl Pts',(15.1,-0.419074661497203,4.29974303548351));
#14044=CARTESIAN_POINT('Ctrl Pts',(15.1,-0.411628924918527,4.30491398987477));
#14045=CARTESIAN_POINT('Ctrl Pts',(15.1,-0.404040271526401,4.30987739070861));
#14046=CARTESIAN_POINT('Ctrl Pts',(15.1,-0.398073367501634,4.31378007737535));
#14047=CARTESIAN_POINT('Ctrl Pts',(15.1,-0.392026704362881,4.31754881952869));
#14048=CARTESIAN_POINT('Ctrl Pts',(15.1,-0.385904261325812,4.32117966642505));
#14049=CARTESIAN_POINT('Ctrl Pts',(15.1,-0.366868686798561,4.33246850264191));
#14050=CARTESIAN_POINT('Ctrl Pts',(15.1,-0.347097727375919,4.34242824684389));
#14051=CARTESIAN_POINT('Ctrl Pts',(15.1,-0.326713262272485,4.3509180109496));
#14052=CARTESIAN_POINT('Ctrl Pts',(15.1,-0.308010762698638,4.35870726657947));
#14053=CARTESIAN_POINT('Ctrl Pts',(15.1,-0.288791261952878,4.36525839133365));
#14054=CARTESIAN_POINT('Ctrl Pts',(15.1,-0.269173508333929,4.37043259773196));
#14055=CARTESIAN_POINT('Ctrl Pts',(12.5,-0.186196943290592,3.58169363627332));
#14056=CARTESIAN_POINT('Ctrl Pts',(12.5,-0.170588484282379,3.56594316788148));
#14057=CARTESIAN_POINT('Ctrl Pts',(12.5,-0.153797667832464,3.55144458439849));
#14058=CARTESIAN_POINT('Ctrl Pts',(12.5,-0.136060690067392,3.53823162417247));
#14059=CARTESIAN_POINT('Ctrl Pts',(12.5,-0.117990710310259,3.5247705978929));
#14060=CARTESIAN_POINT('Ctrl Pts',(12.5,-0.0989385549429972,3.51264262455394));
#14061=CARTESIAN_POINT('Ctrl Pts',(12.5,-0.0790990435859813,3.5018744512649));
#14062=CARTESIAN_POINT('Ctrl Pts',(12.5,-0.0668145727052721,3.49520688224936));
#14063=CARTESIAN_POINT('Ctrl Pts',(12.5,-0.054227138249592,3.4890605701039));
#14064=CARTESIAN_POINT('Ctrl Pts',(12.5,-0.0413735013057162,3.4834433907237));
#14065=CARTESIAN_POINT('Ctrl Pts',(12.5,-0.0353493612034326,3.48081077586818));
#14066=CARTESIAN_POINT('Ctrl Pts',(12.5,-0.0292710672153644,3.47829647656688));
#14067=CARTESIAN_POINT('Ctrl Pts',(12.5,-0.0231507758853709,3.47590397706369));
#14068=CARTESIAN_POINT('Ctrl Pts',(12.5,-0.00211397253512804,3.467680423829));
#14069=CARTESIAN_POINT('Ctrl Pts',(12.5,0.0194422610390746,3.46088402724794));
#14070=CARTESIAN_POINT('Ctrl Pts',(12.5,0.0413436963816045,3.45552737346533));
#14071=CARTESIAN_POINT('Ctrl Pts',(12.5,0.0650920698750741,3.44971899548849));
#14072=CARTESIAN_POINT('Ctrl Pts',(12.5,0.089246474293393,3.44560199012534));
#14073=CARTESIAN_POINT('Ctrl Pts',(12.5,0.113633446029948,3.44311473184586));
#14074=CARTESIAN_POINT('Ctrl Pts',(12.5,0.123118497624279,3.44214733936417));
#14075=CARTESIAN_POINT('Ctrl Pts',(12.5,0.132642564327611,3.44142688205345));
#14076=CARTESIAN_POINT('Ctrl Pts',(12.5,0.142169452875131,3.44095138714122));
#14077=CARTESIAN_POINT('Ctrl Pts',(12.5,0.170359862108328,3.43954438042575));
#14078=CARTESIAN_POINT('Ctrl Pts',(12.5,0.19861482332424,3.44027367679077));
#14079=CARTESIAN_POINT('Ctrl Pts',(12.5,0.226679319731597,3.44302987267532));
#14080=CARTESIAN_POINT('Ctrl Pts',(12.5,0.254743816138955,3.44578606855986));
#14081=CARTESIAN_POINT('Ctrl Pts',(12.5,0.282619254593541,3.45056842907764));
#14082=CARTESIAN_POINT('Ctrl Pts',(12.5,0.310093463203745,3.45730861053194));
#14083=CARTESIAN_POINT('Ctrl Pts',(15.0699957084852,-1.05870731373636E-5,
4.45788944868556));
#14084=CARTESIAN_POINT('Ctrl Pts',(15.0634386537186,0.0628625045491076,
4.45782850550181));
#14085=CARTESIAN_POINT('Ctrl Pts',(15.0568815989521,0.125761012144406,4.44477074790967));
#14086=CARTESIAN_POINT('Ctrl Pts',(15.0503245441856,0.183365120595825,4.41959809737683));
#14087=CARTESIAN_POINT('Ctrl Pts',(15.0424531721356,0.252515583017112,4.38937975928409));
#14088=CARTESIAN_POINT('Ctrl Pts',(15.0345818000857,0.314036477612831,4.34170308552782));
#14089=CARTESIAN_POINT('Ctrl Pts',(15.0267104280357,0.360556892971808,4.28228266426341));
#14090=CARTESIAN_POINT('Ctrl Pts',(15.0188390559858,0.407077308330786,4.222862242999));
#14091=CARTESIAN_POINT('Ctrl Pts',(15.0109676839358,0.438597244453022,4.15169807422645));
#14092=CARTESIAN_POINT('Ctrl Pts',(15.0030963118859,0.45133921416074,4.07731692107955));
#14093=CARTESIAN_POINT('Ctrl Pts',(14.9952249398359,0.464081183868457,4.00293576793266));
#14094=CARTESIAN_POINT('Ctrl Pts',(14.9873535677859,0.458045187161657,3.92533763041141));
#14095=CARTESIAN_POINT('Ctrl Pts',(14.979482195736,0.433954739621328,3.85382131653551));
#14096=CARTESIAN_POINT('Ctrl Pts',(14.971610823686,0.409864292080999,3.78230500265962));
#14097=CARTESIAN_POINT('Ctrl Pts',(14.9637394516361,0.367719393707138,3.71687051242907));
#14098=CARTESIAN_POINT('Ctrl Pts',(14.9558680795861,0.312570095196614,3.66535860215541));
#14099=CARTESIAN_POINT('Ctrl Pts',(14.9479967075362,0.257420796686091,3.61384669188175));
#14100=CARTESIAN_POINT('Ctrl Pts',(14.9401253354862,0.189267098038905,3.57625736156498));
#14101=CARTESIAN_POINT('Ctrl Pts',(14.9322539634362,0.116275803938161,3.55709495786573));
#14102=CARTESIAN_POINT('Ctrl Pts',(14.9243825913863,0.0432845098374172,
3.53793255416647));
#14103=CARTESIAN_POINT('Ctrl Pts',(14.9165112193363,-0.0345443797168851,
3.53719707708475));
#14104=CARTESIAN_POINT('Ctrl Pts',(14.9086398472864,-0.107884770736704,
3.55497662303181));
#14105=CARTESIAN_POINT('Ctrl Pts',(14.9007684752364,-0.181225161756525,
3.57275616897888));
#14106=CARTESIAN_POINT('Ctrl Pts',(14.8928971031865,-0.250077054241862,
3.60905073795473));
#14107=CARTESIAN_POINT('Ctrl Pts',(14.8850257311365,-0.306190019513209,
3.65951122309406));
#14108=CARTESIAN_POINT('Ctrl Pts',(14.8771543590866,-0.362302984784554,
3.70997170823338));
#14109=CARTESIAN_POINT('Ctrl Pts',(14.8692829870366,-0.405677022841909,
3.77459810953617));
#14110=CARTESIAN_POINT('Ctrl Pts',(14.8614116149867,-0.431114693744839,
3.84564633596564));
#14111=CARTESIAN_POINT('Ctrl Pts',(14.8535402429367,-0.45655236464777,3.91669456239511));
#14112=CARTESIAN_POINT('Ctrl Pts',(14.8456688708867,-0.464053668396277,
3.99416461395126));
#14113=CARTESIAN_POINT('Ctrl Pts',(14.8377974988368,-0.452719732759917,
4.06877337558629));
#14114=CARTESIAN_POINT('Ctrl Pts',(14.8299261267868,-0.441385797123556,
4.14338213722132));
#14115=CARTESIAN_POINT('Ctrl Pts',(14.8220547547369,-0.411216622102327,
4.21512960893523));
#14116=CARTESIAN_POINT('Ctrl Pts',(14.8141833826869,-0.365827335221939,
4.27541839855419));
#14117=CARTESIAN_POINT('Ctrl Pts',(14.806312010637,-0.32043804834155,4.33570718817315));
#14118=CARTESIAN_POINT('Ctrl Pts',(14.798440638587,-0.259828649602004,4.38453729569717));
#14119=CARTESIAN_POINT('Ctrl Pts',(14.7905692665371,-0.191261870645823,
4.41605748429924));
#14120=CARTESIAN_POINT('Ctrl Pts',(14.7837114138531,-0.131523763221734,
4.44351912740692));
#14121=CARTESIAN_POINT('Ctrl Pts',(14.7768535611691,-0.065745536276614,
4.45784152413683));
#14122=CARTESIAN_POINT('Ctrl Pts',(14.7699957084852,8.6346448269735E-6,
4.45789857801605));
#14123=CARTESIAN_POINT('Ctrl Pts',(12.5,0.310062960217722,4.54266560670548));
#14124=CARTESIAN_POINT('Ctrl Pts',(12.50787137205,0.220600394030941,4.59378185169648));
#14125=CARTESIAN_POINT('Ctrl Pts',(12.5236141161499,0.0159878432799406,
4.65085692712531));
#14126=CARTESIAN_POINT('Ctrl Pts',(12.5472282322997,-0.294892507759568,
4.580447501361));
#14127=CARTESIAN_POINT('Ctrl Pts',(12.5708423484496,-0.535054221536356,
4.37092866956447));
#14128=CARTESIAN_POINT('Ctrl Pts',(12.5944564645995,-0.647009713430093,
4.07251155115386));
#14129=CARTESIAN_POINT('Ctrl Pts',(12.6180705807493,-0.603894380709874,
3.75671714932517));
#14130=CARTESIAN_POINT('Ctrl Pts',(12.6416846968992,-0.416056506175611,
3.49922677321964));
#14131=CARTESIAN_POINT('Ctrl Pts',(12.6652988130491,-0.128505496873939,
3.36175035317655));
#14132=CARTESIAN_POINT('Ctrl Pts',(12.6889129291989,0.189841674427298,3.37723482234205));
#14133=CARTESIAN_POINT('Ctrl Pts',(12.7125270453488,0.462692468193658,3.54196933898577));
#14134=CARTESIAN_POINT('Ctrl Pts',(12.7361411614987,0.624655556881011,3.81647407445394));
#14135=CARTESIAN_POINT('Ctrl Pts',(12.7597552776485,0.636915702199809,4.13496208375113));
#14136=CARTESIAN_POINT('Ctrl Pts',(12.7833693937984,0.496534514683115,4.42110548633398));
#14137=CARTESIAN_POINT('Ctrl Pts',(12.8069835099483,0.237155397994168,4.60632802944461));
#14138=CARTESIAN_POINT('Ctrl Pts',(12.8305976260981,-0.0790596718614395,
4.64623983861064));
#14139=CARTESIAN_POINT('Ctrl Pts',(12.854211742248,-0.376327535803878,4.5312757721487));
#14140=CARTESIAN_POINT('Ctrl Pts',(12.8778258583979,-0.583405888470749,
4.28898776831928));
#14141=CARTESIAN_POINT('Ctrl Pts',(12.9014399745477,-0.650666957548692,
3.97744183415536));
#14142=CARTESIAN_POINT('Ctrl Pts',(12.9250540906976,-0.561991161265395,
3.67130212143154));
#14143=CARTESIAN_POINT('Ctrl Pts',(12.9486682068475,-0.338630270727757,
3.44393714350224));
#14144=CARTESIAN_POINT('Ctrl Pts',(12.9722823229973,-0.0341142786054444,
3.34983650006563));
#14145=CARTESIAN_POINT('Ctrl Pts',(12.9958964391472,0.278577437919422,3.41155206540036));
#14146=CARTESIAN_POINT('Ctrl Pts',(13.0195105552971,0.524506132150044,3.61429327464512));
#14147=CARTESIAN_POINT('Ctrl Pts',(13.0431246714469,0.644733280558021,3.90947178565704));
#14148=CARTESIAN_POINT('Ctrl Pts',(13.0667387875968,0.61044561006836,4.22634601343335));
#14149=CARTESIAN_POINT('Ctrl Pts',(13.0903529037467,0.429860399609997,4.4889748434194));
#14150=CARTESIAN_POINT('Ctrl Pts',(13.1139670198965,0.146256151980267,4.63441744826062));
#14151=CARTESIAN_POINT('Ctrl Pts',(13.1375811360464,-0.172399400609521,
4.62781749523177));
#14152=CARTESIAN_POINT('Ctrl Pts',(13.1611952521963,-0.449738236712957,
4.47075670902068));
#14153=CARTESIAN_POINT('Ctrl Pts',(13.1848093683461,-0.619294173608025,
4.2008758003961));
#14154=CARTESIAN_POINT('Ctrl Pts',(13.208423484496,-0.64043195068177,3.88285360784221));
#14155=CARTESIAN_POINT('Ctrl Pts',(13.2320376006459,-0.508085752511173,
3.59290636366459));
#14156=CARTESIAN_POINT('Ctrl Pts',(13.2556517167957,-0.253973266794505,
3.40052194335125));
#14157=CARTESIAN_POINT('Ctrl Pts',(13.2792658329456,0.0610056803032868,
3.3518066124833));
#14158=CARTESIAN_POINT('Ctrl Pts',(13.3028799490955,0.361364191435218,3.45843533922715));
#14159=CARTESIAN_POINT('Ctrl Pts',(13.3264940652453,0.575119258511334,3.69485380694));
#14160=CARTESIAN_POINT('Ctrl Pts',(13.3501081813952,0.65104299168552,4.00440268404554));
#14161=CARTESIAN_POINT('Ctrl Pts',(13.3737222975451,0.570939739771795,4.31289642727099));
#14162=CARTESIAN_POINT('Ctrl Pts',(13.3973364136949,0.354006804717113,4.54640236352309));
#14163=CARTESIAN_POINT('Ctrl Pts',(13.4209505298448,0.0522336745508671,
4.6489591696652));
#14164=CARTESIAN_POINT('Ctrl Pts',(13.4445646459947,-0.26205761933777,4.59598839317277));
#14165=CARTESIAN_POINT('Ctrl Pts',(13.4681787621445,-0.513544980480383,
4.40018484937968));
#14166=CARTESIAN_POINT('Ctrl Pts',(13.4917928782944,-0.64195771209056,4.10847422061066));
#14167=CARTESIAN_POINT('Ctrl Pts',(13.5154069944443,-0.616520809113462,
3.79076698974655));
#14168=CARTESIAN_POINT('Ctrl Pts',(13.5390211105941,-0.443330402422436,
3.52320390633144));
#14169=CARTESIAN_POINT('Ctrl Pts',(13.562635226744,-0.163892778617988,3.36990832590288));
#14170=CARTESIAN_POINT('Ctrl Pts',(13.5862493428939,0.154822890495328,3.36761860145296));
#14171=CARTESIAN_POINT('Ctrl Pts',(13.6098634590437,0.43643417612693,3.51688348138565));
#14172=CARTESIAN_POINT('Ctrl Pts',(13.6334775751936,0.613450973283793,3.78193059814177));
#14173=CARTESIAN_POINT('Ctrl Pts',(13.6570916913435,0.643449974253473,4.09923956510808));
#14174=CARTESIAN_POINT('Ctrl Pts',(13.6807058074933,0.519241709620395,4.39276507945606));
#14175=CARTESIAN_POINT('Ctrl Pts',(13.7043199236432,0.270593554659618,4.59216170834183));
#14176=CARTESIAN_POINT('Ctrl Pts',(13.7279340397931,-0.0429042293685969,
4.64964266158552));
#14177=CARTESIAN_POINT('Ctrl Pts',(13.7515481559429,-0.346119716157775,
4.55143222859795));
#14178=CARTESIAN_POINT('Ctrl Pts',(13.7751622720928,-0.566385203513325,
4.32106722332061));
#14179=CARTESIAN_POINT('Ctrl Pts',(13.7987763882427,-0.650912534047929,
4.01375622291695));
#14180=CARTESIAN_POINT('Ctrl Pts',(13.8223905043925,-0.57944414457563,3.70314844792952));
#14181=CARTESIAN_POINT('Ctrl Pts',(13.8460046205424,-0.369107932149097,
3.46368321387984));
#14182=CARTESIAN_POINT('Ctrl Pts',(13.8696187366923,-0.0703124342978696,
3.35275003110641));
#14183=CARTESIAN_POINT('Ctrl Pts',(13.8932328528421,0.245333927901481,3.3969348091043));
#14184=CARTESIAN_POINT('Ctrl Pts',(13.916846968992,0.502184306426786,3.58564835824111));
#14185=CARTESIAN_POINT('Ctrl Pts',(13.9404610851419,0.638682720042094,3.87366416276737));
#14186=CARTESIAN_POINT('Ctrl Pts',(13.9640752012917,0.62211637371287,4.19195723015293));
#14187=CARTESIAN_POINT('Ctrl Pts',(13.9876893174416,0.456455507660852,4.46424641105313));
#14188=CARTESIAN_POINT('Ctrl Pts',(14.0113034335915,0.181401901656729,4.62527570776815));
#14189=CARTESIAN_POINT('Ctrl Pts',(14.0349175497413,-0.137125932879425,
4.63645332836083));
#14190=CARTESIAN_POINT('Ctrl Pts',(14.0585316658912,-0.422790583021024,
4.49510047824495));
#14191=CARTESIAN_POINT('Ctrl Pts',(14.0821457820411,-0.60713052675338,4.23509335195577));
#14192=CARTESIAN_POINT('Ctrl Pts',(14.1057598981909,-0.645967413308333,
3.91874446730605));
#14193=CARTESIAN_POINT('Ctrl Pts',(14.1293740143408,-0.529993712466286,
3.62186903671368));
#14194=CARTESIAN_POINT('Ctrl Pts',(14.1529881304907,-0.287003328966194,
3.41561532377041));
#14195=CARTESIAN_POINT('Ctrl Pts',(14.1766022466405,0.0247694002478971,
3.34941346658496));
#14196=CARTESIAN_POINT('Ctrl Pts',(14.2002163627904,0.330605970264406,3.43912920108534));
#14197=CARTESIAN_POINT('Ctrl Pts',(14.2238304789403,0.557210518047066,3.66326152695696));
#14198=CARTESIAN_POINT('Ctrl Pts',(14.2474445950901,0.650275686248857,3.96809557204375));
#14199=CARTESIAN_POINT('Ctrl Pts',(14.27105871124,0.587497759452106,4.28057573538778));
#14200=CARTESIAN_POINT('Ctrl Pts',(14.2946728273899,0.383921904832036,4.52581397056352));
#14201=CARTESIAN_POINT('Ctrl Pts',(14.3182869435397,0.088336493108731,4.64503722732482));
#14202=CARTESIAN_POINT('Ctrl Pts',(14.3419010596896,-0.22841937412829,4.6096728222354));
#14203=CARTESIAN_POINT('Ctrl Pts',(14.3655151758395,-0.490432948250941,
4.42819608115853));
#14204=CARTESIAN_POINT('Ctrl Pts',(14.3891292919893,-0.634910852255616,
4.14409916841427));
#14205=CARTESIAN_POINT('Ctrl Pts',(14.4127434081392,-0.627227950688033,
3.82546788683648));
#14206=CARTESIAN_POINT('Ctrl Pts',(14.4363575242891,-0.469225504392149,
3.54866444115539));
#14207=CARTESIAN_POINT('Ctrl Pts',(14.4599716404389,-0.198769899531221,
3.38002670405092));
#14208=CARTESIAN_POINT('Ctrl Pts',(14.4835857565888,0.11932229545683,3.35996988316441));
#14209=CARTESIAN_POINT('Ctrl Pts',(14.5071998727387,0.408818071695872,3.49330073524378));
#14210=CARTESIAN_POINT('Ctrl Pts',(14.5308139888885,0.600337751131954,3.74806559342675));
#14211=CARTESIAN_POINT('Ctrl Pts',(14.5544281050384,0.647982309355475,4.06320828594604));
#14212=CARTESIAN_POINT('Ctrl Pts',(14.5780422211883,0.540333396317157,4.36320267272319));
#14213=CARTESIAN_POINT('Ctrl Pts',(14.6016563373381,0.303189823409542,4.57615301060753));
#14214=CARTESIAN_POINT('Ctrl Pts',(14.625270453488,-0.00661530128860875,
4.65102426869959));
#14215=CARTESIAN_POINT('Ctrl Pts',(14.6488845696379,-0.314835022974042,
4.56987302880665));
#14216=CARTESIAN_POINT('Ctrl Pts',(14.6724986857877,-0.547602339746838,
4.35214775046202));
#14217=CARTESIAN_POINT('Ctrl Pts',(14.6961128019376,-0.649132943719538,
4.05002781234082));
#14218=CARTESIAN_POINT('Ctrl Pts',(14.7197269180875,-0.595094318970103,
3.73591836064326));
#14219=CARTESIAN_POINT('Ctrl Pts',(14.7433410342373,-0.398437197867616,
3.48509791236843));
#14220=CARTESIAN_POINT('Ctrl Pts',(14.7669551503872,-0.1062918289807,3.35767733339665));
#14221=CARTESIAN_POINT('Ctrl Pts',(14.7905692665371,0.211327117384507,3.38419385377023));
#14222=CARTESIAN_POINT('Ctrl Pts',(14.8141833826869,0.478300047385911,3.5582926020622));
#14223=CARTESIAN_POINT('Ctrl Pts',(14.8377974988368,0.630645044771057,3.83824960712979));
#14224=CARTESIAN_POINT('Ctrl Pts',(14.8614116149867,0.631851559871185,4.15697121131127));
#14225=CARTESIAN_POINT('Ctrl Pts',(14.8850257311365,0.481630465478622,4.4380735902585));
#14226=CARTESIAN_POINT('Ctrl Pts',(14.9086398472864,0.215983244330552,4.61418854455152));
#14227=CARTESIAN_POINT('Ctrl Pts',(14.9322539634363,-0.101425794369151,
4.64310902247508));
#14228=CARTESIAN_POINT('Ctrl Pts',(14.9558680795861,-0.394527586443172,
4.517903766532));
#14229=CARTESIAN_POINT('Ctrl Pts',(14.979482195736,-0.593077772790822,4.26857965265179));
#14230=CARTESIAN_POINT('Ctrl Pts',(15.0030963118859,-0.649493436571599,
3.95488773069898));
#14231=CARTESIAN_POINT('Ctrl Pts',(15.0267104280357,-0.550252000240565,
3.65200904506483));
#14232=CARTESIAN_POINT('Ctrl Pts',(15.0503245441856,-0.319142060764588,
3.43252503194012));
#14233=CARTESIAN_POINT('Ctrl Pts',(15.0739386603355,-0.0115409051696555,
3.34904846156061));
#14234=CARTESIAN_POINT('Ctrl Pts',(15.0975527764853,0.298810377697559,3.42155963907315));
#14235=CARTESIAN_POINT('Ctrl Pts',(15.1211668926352,0.537575400322941,3.63273573589665));
#14236=CARTESIAN_POINT('Ctrl Pts',(15.1369096367351,0.610790903144771,3.83214323401692));
#14237=CARTESIAN_POINT('Ctrl Pts',(15.1447810087851,0.621570310124627,3.93461384266089));
#14238=CARTESIAN_POINT('Ctrl Pts',(12.4850729970716,0.282426015030316,4.49429601229446));
#14239=CARTESIAN_POINT('Ctrl Pts',(12.4929443691216,0.200937545576316,4.54085609598193));
#14240=CARTESIAN_POINT('Ctrl Pts',(12.5086871132215,0.0145627935155885,
4.59284387968754));
#14241=CARTESIAN_POINT('Ctrl Pts',(12.5323012293714,-0.268607755567932,
4.52871028073968));
#14242=CARTESIAN_POINT('Ctrl Pts',(12.5559153455213,-0.487363055256749,
4.3378665608173));
#14243=CARTESIAN_POINT('Ctrl Pts',(12.5795294616711,-0.589339580973024,
4.06604835489435));
#14244=CARTESIAN_POINT('Ctrl Pts',(12.603143577821,-0.550067261575934,3.77840176074865));
#14245=CARTESIAN_POINT('Ctrl Pts',(12.6267576939709,-0.378972002925158,
3.54386236016666));
#14246=CARTESIAN_POINT('Ctrl Pts',(12.6503718101207,-0.117051373585908,
3.41863967169675));
#14247=CARTESIAN_POINT('Ctrl Pts',(12.6739859262706,0.172920453180012,3.43274395851062));
#14248=CARTESIAN_POINT('Ctrl Pts',(12.6976000424204,0.42145114619533,3.58279513857084));
#14249=CARTESIAN_POINT('Ctrl Pts',(12.7212141585703,0.568977924911017,3.83283235195095));
#14250=CARTESIAN_POINT('Ctrl Pts',(12.7448282747202,0.580145282610399,4.12293246335278));
#14251=CARTESIAN_POINT('Ctrl Pts',(12.76844239087,0.45227673827436,4.38357095065208));
#14252=CARTESIAN_POINT('Ctrl Pts',(12.7920565070199,0.216016946852954,4.55228399108678));
#14253=CARTESIAN_POINT('Ctrl Pts',(12.8156706231698,-0.0720128197761896,
4.58863832766248));
#14254=CARTESIAN_POINT('Ctrl Pts',(12.8392847393196,-0.34278420811256,4.48392139165784));
#14255=CARTESIAN_POINT('Ctrl Pts',(12.8628988554695,-0.531404976945056,
4.26322932523642));
#14256=CARTESIAN_POINT('Ctrl Pts',(12.8865129716194,-0.592670842732518,
3.97945251867098));
#14257=CARTESIAN_POINT('Ctrl Pts',(12.9101270877692,-0.51189901575794,3.70060005900794));
#14258=CARTESIAN_POINT('Ctrl Pts',(12.9337412039191,-0.308447025930223,
3.49350087944474));
#14259=CARTESIAN_POINT('Ctrl Pts',(12.957355320069,-0.0310735592390789,
3.40778774002645));
#14260=CARTESIAN_POINT('Ctrl Pts',(12.9809694362188,0.253746902286204,3.46400239130434));
#14261=CARTESIAN_POINT('Ctrl Pts',(13.0045835523687,0.477755152237737,3.64867260076509));
#14262=CARTESIAN_POINT('Ctrl Pts',(13.0281976685186,0.587266054150949,3.91754086716214));
#14263=CARTESIAN_POINT('Ctrl Pts',(13.0518117846685,0.556034558024266,4.20617103876933));
#14264=CARTESIAN_POINT('Ctrl Pts',(13.0754259008183,0.391545509324759,4.44539088570928));
#14265=CARTESIAN_POINT('Ctrl Pts',(13.0990400169682,0.133219853633759,4.57786970637232));
#14266=CARTESIAN_POINT('Ctrl Pts',(13.122654133118,-0.157032867368526,4.57185802915678));
#14267=CARTESIAN_POINT('Ctrl Pts',(13.1462682492679,-0.409651568547275,
4.42879659435664));
#14268=CARTESIAN_POINT('Ctrl Pts',(13.1698823654178,-0.564094419600429,
4.1829710707208));
#14269=CARTESIAN_POINT('Ctrl Pts',(13.1934964815676,-0.583348116144335,
3.89329525626321));
#14270=CARTESIAN_POINT('Ctrl Pts',(13.2171105977175,-0.462798375770677,
3.62919197644995));
#14271=CARTESIAN_POINT('Ctrl Pts',(13.2407247138674,-0.231335782947555,
3.45395542080054));
#14272=CARTESIAN_POINT('Ctrl Pts',(13.2643388300172,0.055568040665587,3.40958224975729));
#14273=CARTESIAN_POINT('Ctrl Pts',(13.2879529461671,0.329154596505292,3.50670680265737));
#14274=CARTESIAN_POINT('Ctrl Pts',(13.311567062317,0.523856961936024,3.72205250428141));
#14275=CARTESIAN_POINT('Ctrl Pts',(13.3351811784668,0.593013359693284,4.00401025814095));
#14276=CARTESIAN_POINT('Ctrl Pts',(13.3587952946167,0.520049977633468,4.28500692572024));
#14277=CARTESIAN_POINT('Ctrl Pts',(13.3824094107666,0.322452998189994,4.49769969952106));
#14278=CARTESIAN_POINT('Ctrl Pts',(13.4060235269164,0.0475779130258999,
4.59111527567571));
#14279=CARTESIAN_POINT('Ctrl Pts',(13.4296376430663,-0.238699550200797,
4.5428659610613));
#14280=CARTESIAN_POINT('Ctrl Pts',(13.4532517592162,-0.467771004553565,
4.36451503980497));
#14281=CARTESIAN_POINT('Ctrl Pts',(13.476865875366,-0.584737881352888,4.09880555174689));
#14282=CARTESIAN_POINT('Ctrl Pts',(13.5004799915159,-0.561568254327815,
3.80941662539381));
#14283=CARTESIAN_POINT('Ctrl Pts',(13.5240941076658,-0.403814885886516,
3.56570233148043));
#14284=CARTESIAN_POINT('Ctrl Pts',(13.5477082238157,-0.149284468950505,
3.42607049712074));
#14285=CARTESIAN_POINT('Ctrl Pts',(13.5713223399655,0.141023010189178,3.42398486344345));
#14286=CARTESIAN_POINT('Ctrl Pts',(13.5949364561154,0.39753334322815,3.55994526707815));
#14287=CARTESIAN_POINT('Ctrl Pts',(13.6185505722652,0.55877204319843,3.8013678508274));
#14288=CARTESIAN_POINT('Ctrl Pts',(13.6421646884151,0.586097133215014,4.09039401187145));
#14289=CARTESIAN_POINT('Ctrl Pts',(13.665778804565,0.47295996523623,4.35775661870721));
#14290=CARTESIAN_POINT('Ctrl Pts',(13.6893929207148,0.24647464915429,4.53938036140496));
#14291=CARTESIAN_POINT('Ctrl Pts',(13.7130070368647,-0.0390800323908759,
4.59173784568287));
#14292=CARTESIAN_POINT('Ctrl Pts',(13.7366211530146,-0.315268912124245,
4.50228123595558));
#14293=CARTESIAN_POINT('Ctrl Pts',(13.7602352691644,-0.515901402373503,
4.29244943148197));
#14294=CARTESIAN_POINT('Ctrl Pts',(13.7838493853143,-0.59289453017979,4.01253008491428));
#14295=CARTESIAN_POINT('Ctrl Pts',(13.8074635014642,-0.527796356489121,
3.72960781627073));
#14296=CARTESIAN_POINT('Ctrl Pts',(13.831077617614,-0.336208111796874,3.51148691674935));
#14297=CARTESIAN_POINT('Ctrl Pts',(13.8546917337639,-0.0640452526541193,
3.4104415783338));
#14298=CARTESIAN_POINT('Ctrl Pts',(13.8783058499138,0.223466497127862,3.45068801978614));
#14299=CARTESIAN_POINT('Ctrl Pts',(13.9019199660636,0.457422945247278,3.62258090124322));
#14300=CARTESIAN_POINT('Ctrl Pts',(13.9255340822135,0.581754800262342,3.88492489705937));
#14301=CARTESIAN_POINT('Ctrl Pts',(13.9491481983634,0.566665067602596,4.17484744237197));
#14302=CARTESIAN_POINT('Ctrl Pts',(13.9727623145132,0.415770106744681,4.42286658094793));
#14303=CARTESIAN_POINT('Ctrl Pts',(13.9963764306631,0.165232945489059,4.56954279968241));
#14304=CARTESIAN_POINT('Ctrl Pts',(14.019990546813,-0.124903441395439,4.57972412169294));
#14305=CARTESIAN_POINT('Ctrl Pts',(14.0436046629628,-0.385105849054417,
4.45097052228405));
#14306=CARTESIAN_POINT('Ctrl Pts',(14.0672187791127,-0.553014959135429,
4.21413869785145));
#14307=CARTESIAN_POINT('Ctrl Pts',(14.0908328952626,-0.58839018453545,3.92598704378684));
#14308=CARTESIAN_POINT('Ctrl Pts',(14.1144470114124,-0.482753606228458,
3.65557310990793));
#14309=CARTESIAN_POINT('Ctrl Pts',(14.1380611275623,-0.261421765577673,
3.46770347791168));
#14310=CARTESIAN_POINT('Ctrl Pts',(14.1616752437122,0.0225616210391343,
3.40740241293002));
#14311=CARTESIAN_POINT('Ctrl Pts',(14.185289359862,0.301137958114838,3.48912148496193));
#14312=CARTESIAN_POINT('Ctrl Pts',(14.2089034760119,0.507544487205137,3.69327614952086));
#14313=CARTESIAN_POINT('Ctrl Pts',(14.2325175921618,0.592314446747875,3.97093932005559));
#14314=CARTESIAN_POINT('Ctrl Pts',(14.2561317083116,0.535132125826274,4.25556708484021));
#14315=CARTESIAN_POINT('Ctrl Pts',(14.2797458244615,0.349701665714674,4.47894641865396));
#14316=CARTESIAN_POINT('Ctrl Pts',(14.3033599406114,0.0804627670229728,
4.58754290912926));
#14317=CARTESIAN_POINT('Ctrl Pts',(14.3269740567612,-0.208059593914322,
4.55533065134682));
#14318=CARTESIAN_POINT('Ctrl Pts',(14.3505881729111,-0.44671902479684,4.39002953712461));
#14319=CARTESIAN_POINT('Ctrl Pts',(14.374202289061,-0.578319131624566,4.13125512920294));
#14320=CARTESIAN_POINT('Ctrl Pts',(14.3978164052108,-0.571321032683373,
3.84102451585645));
#14321=CARTESIAN_POINT('Ctrl Pts',(14.4214305213607,-0.427401871100662,
3.58889348396707));
#14322=CARTESIAN_POINT('Ctrl Pts',(14.4450446375106,-0.181052875819672,
3.43528699049651));
#14323=CARTESIAN_POINT('Ctrl Pts',(14.4686587536604,0.108686701521778,3.41701790091169));
#14324=CARTESIAN_POINT('Ctrl Pts',(14.4922728698103,0.372378754238714,3.53846452970905));
#14325=CARTESIAN_POINT('Ctrl Pts',(14.5158869859602,0.546827646247725,3.77052134686598));
#14326=CARTESIAN_POINT('Ctrl Pts',(14.53950110211,0.59022548618159,4.05757432072539));
#14327=CARTESIAN_POINT('Ctrl Pts',(14.5631152182599,0.492171679592087,4.3308292078278));
#14328=CARTESIAN_POINT('Ctrl Pts',(14.5867293344098,0.276165503816305,4.52479857226205));
#14329=CARTESIAN_POINT('Ctrl Pts',(14.6103434505596,-0.00602565743375084,
4.59299630554951));
#14330=CARTESIAN_POINT('Ctrl Pts',(14.6339575667095,-0.286772727926288,
4.51907834617235));
#14331=CARTESIAN_POINT('Ctrl Pts',(14.6575716828594,-0.49879271786407,4.32075964763751));
#14332=CARTESIAN_POINT('Ctrl Pts',(14.6811857990092,-0.591273560669336,
4.04556866666751));
#14333=CARTESIAN_POINT('Ctrl Pts',(14.7047999151591,-0.542051578672567,
3.75945683743125));
#14334=CARTESIAN_POINT('Ctrl Pts',(14.728414031309,-0.362923162297683,3.53099285177933));
#14335=CARTESIAN_POINT('Ctrl Pts',(14.7520281474588,-0.0968176839575538,
3.41492969374656));
#14336=CARTESIAN_POINT('Ctrl Pts',(14.7756422636087,0.192490826988301,3.43908270827084));
#14337=CARTESIAN_POINT('Ctrl Pts',(14.7992563797586,0.435667569828913,3.59766345479839));
#14338=CARTESIAN_POINT('Ctrl Pts',(14.8228704959084,0.574433549780463,3.85266695881428));
#14339=CARTESIAN_POINT('Ctrl Pts',(14.8464846120583,0.575532524168,4.14297984400973));
#14340=CARTESIAN_POINT('Ctrl Pts',(14.8700987282082,0.438701136655627,4.39902663091346));
#14341=CARTESIAN_POINT('Ctrl Pts',(14.893712844358,0.196731937819222,4.55944387228049));
#14342=CARTESIAN_POINT('Ctrl Pts',(14.9173269605079,-0.0923853752310475,
4.58578657160514));
#14343=CARTESIAN_POINT('Ctrl Pts',(14.9409410766578,-0.359362027571537,
4.47174127747511));
#14344=CARTESIAN_POINT('Ctrl Pts',(14.9645551928076,-0.540214773976066,
4.24464025294543));
#14345=CARTESIAN_POINT('Ctrl Pts',(14.9881693089575,-0.59160192159185,3.95890873763601));
#14346=CARTESIAN_POINT('Ctrl Pts',(15.0117834251074,-0.501206205285789,
3.68302663884805));
#14347=CARTESIAN_POINT('Ctrl Pts',(15.0353975412572,-0.290695865081771,
3.48310596742652));
#14348=CARTESIAN_POINT('Ctrl Pts',(15.0590116574071,-0.0105122258222001,
3.40706994202017));
#14349=CARTESIAN_POINT('Ctrl Pts',(15.082625773557,0.272176412698783,3.47311795657709));
#14350=CARTESIAN_POINT('Ctrl Pts',(15.1062398897068,0.489659512974156,3.66547122397039));
#14351=CARTESIAN_POINT('Ctrl Pts',(15.1219826338067,0.5563490739778,3.84710486709154));
#14352=CARTESIAN_POINT('Ctrl Pts',(15.1298540058567,0.566167676482186,3.94044192881839));
#14353=CARTESIAN_POINT('Ctrl Pts',(12.4701459941433,0.254789069842909,4.44592641788345));
#14354=CARTESIAN_POINT('Ctrl Pts',(12.4780173661933,0.181274697121691,4.48793034026739));
#14355=CARTESIAN_POINT('Ctrl Pts',(12.4937601102932,0.0131377437512366,
4.53483083224977));
#14356=CARTESIAN_POINT('Ctrl Pts',(12.517374226443,-0.242323003376296,4.47697306011837));
#14357=CARTESIAN_POINT('Ctrl Pts',(12.5409883425929,-0.439671888977142,
4.30480445207012));
#14358=CARTESIAN_POINT('Ctrl Pts',(12.5646024587428,-0.531669448515955,
4.05958515863483));
#14359=CARTESIAN_POINT('Ctrl Pts',(12.5882165748926,-0.496240142441994,
3.80008637217214));
#14360=CARTESIAN_POINT('Ctrl Pts',(12.6118306910425,-0.341887499674706,
3.58849794711368));
#14361=CARTESIAN_POINT('Ctrl Pts',(12.6354448071924,-0.105597250297878,
3.47552899021694));
#14362=CARTESIAN_POINT('Ctrl Pts',(12.6590589233422,0.155999231932725,3.4882530946792));
#14363=CARTESIAN_POINT('Ctrl Pts',(12.6826730394921,0.380209824197002,3.62362093815591));
#14364=CARTESIAN_POINT('Ctrl Pts',(12.706287155642,0.513300292941022,3.84919062944795));
#14365=CARTESIAN_POINT('Ctrl Pts',(12.7299012717918,0.52337486302099,4.11090284295443));
#14366=CARTESIAN_POINT('Ctrl Pts',(12.7535153879417,0.408018961865605,4.34603641497018));
#14367=CARTESIAN_POINT('Ctrl Pts',(12.7771295040916,0.194878495711741,4.49823995272895));
#14368=CARTESIAN_POINT('Ctrl Pts',(12.8007436202414,-0.0649659676909401,
4.53103681671432));
#14369=CARTESIAN_POINT('Ctrl Pts',(12.8243577363913,-0.30924088042124,4.43656701116699));
#14370=CARTESIAN_POINT('Ctrl Pts',(12.8479718525412,-0.479404065419363,
4.23747088215356));
#14371=CARTESIAN_POINT('Ctrl Pts',(12.871585968691,-0.534674727916345,3.9814632031866));
#14372=CARTESIAN_POINT('Ctrl Pts',(12.8952000848409,-0.461806870250484,
3.72989799658434));
#14373=CARTESIAN_POINT('Ctrl Pts',(12.9188142009908,-0.278263781132688,
3.54306461538724));
#14374=CARTESIAN_POINT('Ctrl Pts',(12.9424283171406,-0.0280328398727138,
3.46573897998727));
#14375=CARTESIAN_POINT('Ctrl Pts',(12.9660424332905,0.228916366652986,3.51645271720832));
#14376=CARTESIAN_POINT('Ctrl Pts',(12.9896565494404,0.431004172325429,3.68305192688505));
#14377=CARTESIAN_POINT('Ctrl Pts',(13.0132706655902,0.529798827743877,3.92560994866724));
#14378=CARTESIAN_POINT('Ctrl Pts',(13.0368847817401,0.501623505980173,4.1859960641053));
#14379=CARTESIAN_POINT('Ctrl Pts',(13.06049889789,0.353230619039521,4.40180692799916));
#14380=CARTESIAN_POINT('Ctrl Pts',(13.0841130140398,0.120183555287252,4.52132196448402));
#14381=CARTESIAN_POINT('Ctrl Pts',(13.1077271301897,-0.14166633412753,4.51589856308179));
#14382=CARTESIAN_POINT('Ctrl Pts',(13.1313412463396,-0.369564900381594,
4.38683647969259));
#14383=CARTESIAN_POINT('Ctrl Pts',(13.1549553624894,-0.508894665592834,
4.16506634104549));
#14384=CARTESIAN_POINT('Ctrl Pts',(13.1785694786393,-0.5262642816069,3.9037369046842));
#14385=CARTESIAN_POINT('Ctrl Pts',(13.2021835947892,-0.417510999030181,
3.66547758923531));
#14386=CARTESIAN_POINT('Ctrl Pts',(13.225797710939,-0.208698299100604,3.50738889824983));
#14387=CARTESIAN_POINT('Ctrl Pts',(13.2494118270889,0.0501304010278875,
3.46735788703128));
#14388=CARTESIAN_POINT('Ctrl Pts',(13.2730259432388,0.296945001575366,3.55497826608759));
#14389=CARTESIAN_POINT('Ctrl Pts',(13.2966400593886,0.472594665360713,3.74925120162283));
#14390=CARTESIAN_POINT('Ctrl Pts',(13.3202541755385,0.534983727701048,4.00361783223636));
#14391=CARTESIAN_POINT('Ctrl Pts',(13.3438682916884,0.469160215495142,4.25711742416948));
#14392=CARTESIAN_POINT('Ctrl Pts',(13.3674824078382,0.290899191662876,4.44899703551904));
#14393=CARTESIAN_POINT('Ctrl Pts',(13.3910965239881,0.0429221515009326,
4.53327138168622));
#14394=CARTESIAN_POINT('Ctrl Pts',(13.414710640138,-0.215341481063824,4.48974352894983));
#14395=CARTESIAN_POINT('Ctrl Pts',(13.4383247562878,-0.421997028626747,
4.32884523023027));
#14396=CARTESIAN_POINT('Ctrl Pts',(13.4619388724377,-0.527518050615216,
4.08913688288313));
#14397=CARTESIAN_POINT('Ctrl Pts',(13.4855529885876,-0.506615699542168,
3.82806626104107));
#14398=CARTESIAN_POINT('Ctrl Pts',(13.5091671047374,-0.364299369350597,
3.60820075662942));
#14399=CARTESIAN_POINT('Ctrl Pts',(13.5327812208873,-0.134676159283021,
3.48223266833859));
#14400=CARTESIAN_POINT('Ctrl Pts',(13.5563953370372,0.127223129883027,3.48035112543394));
#14401=CARTESIAN_POINT('Ctrl Pts',(13.580009453187,0.35863251032937,3.60300705277064));
#14402=CARTESIAN_POINT('Ctrl Pts',(13.6036235693369,0.504093113113068,3.82080510351303));
#14403=CARTESIAN_POINT('Ctrl Pts',(13.6272376854868,0.528744292176554,4.08154845863482));
#14404=CARTESIAN_POINT('Ctrl Pts',(13.6508518016366,0.426678220852065,4.32274815795836));
#14405=CARTESIAN_POINT('Ctrl Pts',(13.6744659177865,0.222355743648963,4.48659901446809));
#14406=CARTESIAN_POINT('Ctrl Pts',(13.6980800339364,-0.0352558354131549,
4.53383302978021));
#14407=CARTESIAN_POINT('Ctrl Pts',(13.7216941500862,-0.284418108090716,
4.45313024331322));
#14408=CARTESIAN_POINT('Ctrl Pts',(13.7453082662361,-0.465417601233682,
4.26383163964332));
#14409=CARTESIAN_POINT('Ctrl Pts',(13.768922382386,-0.534876526311652,4.01130394691162));
#14410=CARTESIAN_POINT('Ctrl Pts',(13.7925364985358,-0.476148568402614,
3.75606718461195));
#14411=CARTESIAN_POINT('Ctrl Pts',(13.8161506146857,-0.303308291444651,
3.55929061961886));
#14412=CARTESIAN_POINT('Ctrl Pts',(13.8397647308356,-0.0577780710103693,
3.46813312556118));
#14413=CARTESIAN_POINT('Ctrl Pts',(13.8633788469854,0.201599066354243,3.50444123046797));
#14414=CARTESIAN_POINT('Ctrl Pts',(13.8869929631353,0.412661584067771,3.65951344424533));
#14415=CARTESIAN_POINT('Ctrl Pts',(13.9106070792852,0.52482688048259,3.89618563135138));
#14416=CARTESIAN_POINT('Ctrl Pts',(13.934221195435,0.511213761492322,4.157737654591));
#14417=CARTESIAN_POINT('Ctrl Pts',(13.9578353115849,0.375084705828511,4.38148675084272));
#14418=CARTESIAN_POINT('Ctrl Pts',(13.9814494277348,0.149063989321389,4.51380989159668));
#14419=CARTESIAN_POINT('Ctrl Pts',(14.0050635438846,-0.112680949911453,
4.52299491502504));
#14420=CARTESIAN_POINT('Ctrl Pts',(14.0286776600345,-0.347421115087809,
4.40684056632315));
#14421=CARTESIAN_POINT('Ctrl Pts',(14.0522917761844,-0.498899391517477,
4.19318404374712));
#14422=CARTESIAN_POINT('Ctrl Pts',(14.0759058923342,-0.530812955762567,
3.93322962026762));
#14423=CARTESIAN_POINT('Ctrl Pts',(14.0995200084841,-0.435513499990629,
3.68927718310219));
#14424=CARTESIAN_POINT('Ctrl Pts',(14.123134124634,-0.235840202189154,3.51979163205294));
#14425=CARTESIAN_POINT('Ctrl Pts',(14.1467482407838,0.020353841830372,3.46539135927508));
#14426=CARTESIAN_POINT('Ctrl Pts',(14.1703623569337,0.271669945965271,3.53911376883853));
#14427=CARTESIAN_POINT('Ctrl Pts',(14.1939764730836,0.457878456363209,3.72329077208477));
#14428=CARTESIAN_POINT('Ctrl Pts',(14.2175905892334,0.534353207246894,3.97378306806742));
#14429=CARTESIAN_POINT('Ctrl Pts',(14.2412047053833,0.482766492200443,4.23055843429265));
#14430=CARTESIAN_POINT('Ctrl Pts',(14.2648188215332,0.315481426597312,4.4320788667444));
#14431=CARTESIAN_POINT('Ctrl Pts',(14.288432937683,0.0725890409372144,4.53004859093371));
#14432=CARTESIAN_POINT('Ctrl Pts',(14.3120470538329,-0.187699813700353,
4.50098848045824));
#14433=CARTESIAN_POINT('Ctrl Pts',(14.3356611699828,-0.40300510134274,4.35186299309067));
#14434=CARTESIAN_POINT('Ctrl Pts',(14.3592752861326,-0.521727410993515,
4.11841108999162));
#14435=CARTESIAN_POINT('Ctrl Pts',(14.3828894022825,-0.515414114678713,
3.85658114487643));
#14436=CARTESIAN_POINT('Ctrl Pts',(14.4065035184324,-0.385578237809175,
3.62912252677875));
#14437=CARTESIAN_POINT('Ctrl Pts',(14.4301176345822,-0.163335852108122,
3.49054727694211));
#14438=CARTESIAN_POINT('Ctrl Pts',(14.4537317507321,0.0980511075867261,
3.47406591865897));
#14439=CARTESIAN_POINT('Ctrl Pts',(14.477345866882,0.335939436781555,3.58362832417432));
#14440=CARTESIAN_POINT('Ctrl Pts',(14.5009599830318,0.493317541363497,3.79297710030521));
#14441=CARTESIAN_POINT('Ctrl Pts',(14.5245740991817,0.532468663007706,4.05194035550473));
#14442=CARTESIAN_POINT('Ctrl Pts',(14.5481882153316,0.444009962867018,4.2984557429324));
#14443=CARTESIAN_POINT('Ctrl Pts',(14.5718023314814,0.249141184223067,4.47344413391656));
#14444=CARTESIAN_POINT('Ctrl Pts',(14.5954164476313,-0.00543601357889273,
4.53496834239941));
#14445=CARTESIAN_POINT('Ctrl Pts',(14.6190305637812,-0.258710432878536,
4.46828366353805));
#14446=CARTESIAN_POINT('Ctrl Pts',(14.642644679931,-0.449983095981302,4.28937154481299));
#14447=CARTESIAN_POINT('Ctrl Pts',(14.6662587960809,-0.533414177619135,
4.0411095209942));
#14448=CARTESIAN_POINT('Ctrl Pts',(14.6898729122308,-0.489008838375032,
3.78299531421925));
#14449=CARTESIAN_POINT('Ctrl Pts',(14.7134870283806,-0.327409126727749,
3.57688779119022));
#14450=CARTESIAN_POINT('Ctrl Pts',(14.7371011445305,-0.0873435389344073,
3.47218205409647));
#14451=CARTESIAN_POINT('Ctrl Pts',(14.7607152606804,0.173654536592096,3.49397156277145));
#14452=CARTESIAN_POINT('Ctrl Pts',(14.7843293768302,0.393035092271916,3.63703430753458));
#14453=CARTESIAN_POINT('Ctrl Pts',(14.8079434929801,0.518222054789869,3.86708431049878));
#14454=CARTESIAN_POINT('Ctrl Pts',(14.8315576091299,0.519213488464815,4.12898847670818));
#14455=CARTESIAN_POINT('Ctrl Pts',(14.8551717252798,0.395771807832633,4.35997967156842));
#14456=CARTESIAN_POINT('Ctrl Pts',(14.8787858414297,0.177480631307892,4.50469920000947));
#14457=CARTESIAN_POINT('Ctrl Pts',(14.9023999575796,-0.0833449560929437,
4.52846412073519));
#14458=CARTESIAN_POINT('Ctrl Pts',(14.9260140737294,-0.324196468699902,
4.42557878841823));
#14459=CARTESIAN_POINT('Ctrl Pts',(14.9496281898793,-0.487351775161311,
4.22070085323907));
#14460=CARTESIAN_POINT('Ctrl Pts',(14.9732423060292,-0.533710406612102,
3.96292974457304));
#14461=CARTESIAN_POINT('Ctrl Pts',(14.996856422179,-0.452160410331013,3.71404423263127));
#14462=CARTESIAN_POINT('Ctrl Pts',(15.0204705383289,-0.262249669398955,
3.53368690291293));
#14463=CARTESIAN_POINT('Ctrl Pts',(15.0440846544788,-0.0094835464747447,
3.46509142247974));
#14464=CARTESIAN_POINT('Ctrl Pts',(15.0676987706286,0.245542447700007,3.52467627408104));
#14465=CARTESIAN_POINT('Ctrl Pts',(15.0913128867785,0.441743625625371,3.69820671204414));
#14466=CARTESIAN_POINT('Ctrl Pts',(15.1070556308784,0.501907244810829,3.86206650016617));
#14467=CARTESIAN_POINT('Ctrl Pts',(15.1149270029284,0.510765042839744,3.94627001497588));
#14468=CARTESIAN_POINT('Ctrl Pts',(12.4552189912149,0.227152124655503,4.39755682347243));
#14469=CARTESIAN_POINT('Ctrl Pts',(12.4630903632649,0.161611848667067,4.43500458455284));
#14470=CARTESIAN_POINT('Ctrl Pts',(12.4788331073648,0.0117126939868845,
4.476817784812));
#14471=CARTESIAN_POINT('Ctrl Pts',(12.5024472235147,-0.216038251184659,
4.42523583949706));
#14472=CARTESIAN_POINT('Ctrl Pts',(12.5260613396645,-0.391980722697534,
4.27174234332294));
#14473=CARTESIAN_POINT('Ctrl Pts',(12.5496754558144,-0.473999316058885,
4.05312196237532));
#14474=CARTESIAN_POINT('Ctrl Pts',(12.5732895719643,-0.442413023308054,
3.82177098359562));
#14475=CARTESIAN_POINT('Ctrl Pts',(12.5969036881141,-0.304802996424253,
3.6331335340607));
#14476=CARTESIAN_POINT('Ctrl Pts',(12.620517804264,-0.0941431270098475,
3.53241830873714));
#14477=CARTESIAN_POINT('Ctrl Pts',(12.6441319204139,0.139078010685439,3.54376223084778));
#14478=CARTESIAN_POINT('Ctrl Pts',(12.6677460365637,0.338968502198674,3.66444673774097));
#14479=CARTESIAN_POINT('Ctrl Pts',(12.6913601527136,0.457622660971028,3.86554890694496));
#14480=CARTESIAN_POINT('Ctrl Pts',(12.7149742688635,0.46660444343158,4.09887322255608));
#14481=CARTESIAN_POINT('Ctrl Pts',(12.7385883850133,0.36376118545685,4.30850187928827));
#14482=CARTESIAN_POINT('Ctrl Pts',(12.7622025011632,0.173740044570527,4.44419591437112));
#14483=CARTESIAN_POINT('Ctrl Pts',(12.7858166173131,-0.0579191156056905,
4.47343530576616));
#14484=CARTESIAN_POINT('Ctrl Pts',(12.809430733463,-0.275697552729921,4.38921263067613));
#14485=CARTESIAN_POINT('Ctrl Pts',(12.8330448496128,-0.42740315389367,4.2117124390707));
#14486=CARTESIAN_POINT('Ctrl Pts',(12.8566589657627,-0.476678613100171,
3.98347388770222));
#14487=CARTESIAN_POINT('Ctrl Pts',(12.8802730819125,-0.411714724743029,
3.75919593416074));
#14488=CARTESIAN_POINT('Ctrl Pts',(12.9038871980624,-0.248080536335154,
3.59262835132974));
#14489=CARTESIAN_POINT('Ctrl Pts',(12.9275013142123,-0.0249921205063485,
3.52369021994808));
#14490=CARTESIAN_POINT('Ctrl Pts',(12.9511154303621,0.204085831019768,3.5689030431123));
#14491=CARTESIAN_POINT('Ctrl Pts',(12.974729546512,0.384253192413122,3.71743125300502));
#14492=CARTESIAN_POINT('Ctrl Pts',(12.9983436626619,0.472331601336806,3.93367903017235));
#14493=CARTESIAN_POINT('Ctrl Pts',(13.0219577788117,0.44721245393608,4.16582108944128));
#14494=CARTESIAN_POINT('Ctrl Pts',(13.0455718949616,0.314915728754283,4.35822297028905));
#14495=CARTESIAN_POINT('Ctrl Pts',(13.0691860111115,0.107147256940744,4.46477422259573));
#14496=CARTESIAN_POINT('Ctrl Pts',(13.0928001272613,-0.126299800886535,
4.4599390970068));
#14497=CARTESIAN_POINT('Ctrl Pts',(13.1164142434112,-0.329478232215912,
4.34487636502855));
#14498=CARTESIAN_POINT('Ctrl Pts',(13.1400283595611,-0.453694911585238,
4.14716161137019));
#14499=CARTESIAN_POINT('Ctrl Pts',(13.1636424757109,-0.469180447069464,
3.9141785531052));
#14500=CARTESIAN_POINT('Ctrl Pts',(13.1872565918608,-0.372223622289685,
3.70176320202068));
#14501=CARTESIAN_POINT('Ctrl Pts',(13.2108707080107,-0.186060815253654,
3.56082237569912));
#14502=CARTESIAN_POINT('Ctrl Pts',(13.2344848241605,0.0446927613901878,
3.52513352430527));
#14503=CARTESIAN_POINT('Ctrl Pts',(13.2580989403104,0.26473540664544,3.60324972951781));
#14504=CARTESIAN_POINT('Ctrl Pts',(13.2817130564603,0.421332368785403,3.77644989896424));
#14505=CARTESIAN_POINT('Ctrl Pts',(13.3053271726101,0.476954095708811,4.00322540633176));
#14506=CARTESIAN_POINT('Ctrl Pts',(13.32894128876,0.418270453356816,4.22922792261873));
#14507=CARTESIAN_POINT('Ctrl Pts',(13.3525554049099,0.259345385135757,4.40029437151701));
#14508=CARTESIAN_POINT('Ctrl Pts',(13.3761695210597,0.0382663899759653,
4.47542748769673));
#14509=CARTESIAN_POINT('Ctrl Pts',(13.3997836372096,-0.19198341192685,4.43662109683837));
#14510=CARTESIAN_POINT('Ctrl Pts',(13.4233977533595,-0.376223052699929,
4.29317542065556));
#14511=CARTESIAN_POINT('Ctrl Pts',(13.4470118695093,-0.470298219877544,
4.07946821401937));
#14512=CARTESIAN_POINT('Ctrl Pts',(13.4706259856592,-0.451663144756522,
3.84671589668833));
#14513=CARTESIAN_POINT('Ctrl Pts',(13.4942401018091,-0.324783852814677,
3.65069918177841));
#14514=CARTESIAN_POINT('Ctrl Pts',(13.5178542179589,-0.120067849615538,
3.53839483955645));
#14515=CARTESIAN_POINT('Ctrl Pts',(13.5414683341088,0.113423249576877,3.53671738742444));
#14516=CARTESIAN_POINT('Ctrl Pts',(13.5650824502587,0.319731677430589,3.64606883846313));
#14517=CARTESIAN_POINT('Ctrl Pts',(13.5886965664085,0.449414183027706,3.84024235619866));
#14518=CARTESIAN_POINT('Ctrl Pts',(13.6123106825584,0.471391451138094,4.07270290539818));
#14519=CARTESIAN_POINT('Ctrl Pts',(13.6359247987083,0.380396476467901,4.28773969720951));
#14520=CARTESIAN_POINT('Ctrl Pts',(13.6595389148581,0.198236838143636,4.43381766753122));
#14521=CARTESIAN_POINT('Ctrl Pts',(13.683153031008,-0.0314316384354341,
4.47592821387755));
#14522=CARTESIAN_POINT('Ctrl Pts',(13.7067671471579,-0.253567304057185,
4.40397925067086));
#14523=CARTESIAN_POINT('Ctrl Pts',(13.7303812633077,-0.414933800093862,
4.23521384780468));
#14524=CARTESIAN_POINT('Ctrl Pts',(13.7539953794576,-0.476858522443512,
4.01007780890896));
#14525=CARTESIAN_POINT('Ctrl Pts',(13.7776094956075,-0.424500780316106,
3.78252655295316));
#14526=CARTESIAN_POINT('Ctrl Pts',(13.8012236117573,-0.270408471092428,
3.60709432248837));
#14527=CARTESIAN_POINT('Ctrl Pts',(13.8248377279072,-0.0515108893666192,
3.52582467278856));
#14528=CARTESIAN_POINT('Ctrl Pts',(13.8484518440571,0.179731635580624,3.55819444114981));
#14529=CARTESIAN_POINT('Ctrl Pts',(13.8720659602069,0.367900222888263,3.69644598724744));
#14530=CARTESIAN_POINT('Ctrl Pts',(13.8956800763568,0.467898960702838,3.90744636564338));
#14531=CARTESIAN_POINT('Ctrl Pts',(13.9192941925067,0.455762455382048,4.14062786681004));
#14532=CARTESIAN_POINT('Ctrl Pts',(13.9429083086565,0.33439930491234,4.34010692073752));
#14533=CARTESIAN_POINT('Ctrl Pts',(13.9665224248064,0.132895033153719,4.45807698351094));
#14534=CARTESIAN_POINT('Ctrl Pts',(13.9901365409563,-0.100458458427467,
4.46626570835715));
#14535=CARTESIAN_POINT('Ctrl Pts',(14.0137506571061,-0.309736381121202,
4.36271061036225));
#14536=CARTESIAN_POINT('Ctrl Pts',(14.037364773256,-0.444783823899526,4.1722293896428));
#14537=CARTESIAN_POINT('Ctrl Pts',(14.0609788894059,-0.473235726989685,
3.94047219674841));
#14538=CARTESIAN_POINT('Ctrl Pts',(14.0845930055557,-0.388273393752801,
3.72298125629644));
#14539=CARTESIAN_POINT('Ctrl Pts',(14.1082071217056,-0.210258638800633,
3.5718797861942));
#14540=CARTESIAN_POINT('Ctrl Pts',(14.1318212378555,0.0181460626216094,
3.52338030562014));
#14541=CARTESIAN_POINT('Ctrl Pts',(14.1554353540053,0.242201933815703,3.58910605271512));
#14542=CARTESIAN_POINT('Ctrl Pts',(14.1790494701552,0.40821242552128,3.75330539464867));
#14543=CARTESIAN_POINT('Ctrl Pts',(14.2026635863051,0.476391967745912,3.97662681607925));
#14544=CARTESIAN_POINT('Ctrl Pts',(14.2262777024549,0.430400858574612,4.20554978374509));
#14545=CARTESIAN_POINT('Ctrl Pts',(14.2498918186048,0.28126118747995,4.38521131483484));
#14546=CARTESIAN_POINT('Ctrl Pts',(14.2735059347547,0.0647153148514563,
4.47255427273816));
#14547=CARTESIAN_POINT('Ctrl Pts',(14.2971200509045,-0.167340033486385,
4.44664630956965));
#14548=CARTESIAN_POINT('Ctrl Pts',(14.3207341670544,-0.359291177888639,
4.31369644905674));
#14549=CARTESIAN_POINT('Ctrl Pts',(14.3443482832043,-0.465135690362464,
4.10556705078029));
#14550=CARTESIAN_POINT('Ctrl Pts',(14.3679623993541,-0.459507196674052,
3.87213777389641));
#14551=CARTESIAN_POINT('Ctrl Pts',(14.391576515504,-0.343754604517688,3.66935156959044));
#14552=CARTESIAN_POINT('Ctrl Pts',(14.4151906316539,-0.145618828396573,
3.5458075633877));
#14553=CARTESIAN_POINT('Ctrl Pts',(14.4388047478037,0.0874155136516737,
3.53111393640625));
#14554=CARTESIAN_POINT('Ctrl Pts',(14.4624188639536,0.299500119324396,3.6287921186396));
#14555=CARTESIAN_POINT('Ctrl Pts',(14.4860329801035,0.439807436479269,3.81543285374444));
#14556=CARTESIAN_POINT('Ctrl Pts',(14.5096470962533,0.474711839833821,4.04630639028407));
#14557=CARTESIAN_POINT('Ctrl Pts',(14.5332612124032,0.395848246141948,4.26608227803701));
#14558=CARTESIAN_POINT('Ctrl Pts',(14.5568753285531,0.22211686462983,4.42208969557108));
#14559=CARTESIAN_POINT('Ctrl Pts',(14.5804894447029,-0.00484636972403486,
4.47694037924932));
#14560=CARTESIAN_POINT('Ctrl Pts',(14.6041035608528,-0.230648137830783,
4.41748898090375));
#14561=CARTESIAN_POINT('Ctrl Pts',(14.6277176770027,-0.401173474098533,
4.25798344198848));
#14562=CARTESIAN_POINT('Ctrl Pts',(14.6513317931525,-0.475554794568933,
4.03665037532088));
#14563=CARTESIAN_POINT('Ctrl Pts',(14.6749459093024,-0.435966098077497,
3.80653379100725));
#14564=CARTESIAN_POINT('Ctrl Pts',(14.6985600254523,-0.291895091157815,
3.62278273060111));
#14565=CARTESIAN_POINT('Ctrl Pts',(14.7221741416021,-0.077869393911261,
3.52943441444639));
#14566=CARTESIAN_POINT('Ctrl Pts',(14.745788257752,0.15481824619589,3.54886041727207));
#14567=CARTESIAN_POINT('Ctrl Pts',(14.7694023739019,0.350402614714918,3.67640516027076));
#14568=CARTESIAN_POINT('Ctrl Pts',(14.7930164900517,0.462010559799276,3.88150166218328));
#14569=CARTESIAN_POINT('Ctrl Pts',(14.8166306062016,0.46289445276163,4.11499710940664));
#14570=CARTESIAN_POINT('Ctrl Pts',(14.8402447223515,0.352842479009638,4.32093271222338));
#14571=CARTESIAN_POINT('Ctrl Pts',(14.8638588385013,0.158229324796562,4.44995452773844));
#14572=CARTESIAN_POINT('Ctrl Pts',(14.8874729546512,-0.07430453695484,4.47114166986524));
#14573=CARTESIAN_POINT('Ctrl Pts',(14.9110870708011,-0.289030909828268,
4.37941629936134));
#14574=CARTESIAN_POINT('Ctrl Pts',(14.9347011869509,-0.434488776346555,
4.1967614535327));
#14575=CARTESIAN_POINT('Ctrl Pts',(14.9583153031008,-0.475818891632353,
3.96695075151007));
#14576=CARTESIAN_POINT('Ctrl Pts',(14.9819294192507,-0.403114615376237,
3.74506182641449));
#14577=CARTESIAN_POINT('Ctrl Pts',(15.0055435354005,-0.233803473716137,
3.58426783839933));
#14578=CARTESIAN_POINT('Ctrl Pts',(15.0291576515504,-0.00845486712728951,
3.5231129029393));
#14579=CARTESIAN_POINT('Ctrl Pts',(15.0527717677003,0.218908482701231,3.57623459158499));
#14580=CARTESIAN_POINT('Ctrl Pts',(15.0763858838501,0.393827738276586,3.73094220011788));
#14581=CARTESIAN_POINT('Ctrl Pts',(15.09212862795,0.447465415643859,3.87702813324079));
#14582=CARTESIAN_POINT('Ctrl Pts',(15.1,0.455362409197302,3.95209810113337));
#14583=CARTESIAN_POINT('',(15.1,0.455362409197302,3.95209810113338));
#14584=CARTESIAN_POINT('Ctrl Pts',(15.1,0.455362409197302,3.95209810113337));
#14585=CARTESIAN_POINT('Ctrl Pts',(15.1,0.461198486074795,3.93070554260298));
#14586=CARTESIAN_POINT('Ctrl Pts',(15.1,0.46535922191849,3.9089149747703));
#14587=CARTESIAN_POINT('Ctrl Pts',(15.1,0.467933495509747,3.88694781877637));
#14588=CARTESIAN_POINT('Ctrl Pts',(15.1,0.470556099470815,3.86456824322593));
#14589=CARTESIAN_POINT('Ctrl Pts',(15.1,0.471533159003394,3.84200460508655));
#14590=CARTESIAN_POINT('Ctrl Pts',(15.1,0.470938919222204,3.8194389967166));
#14591=CARTESIAN_POINT('Ctrl Pts',(15.1,0.470570970565677,3.80546654730098));
#14592=CARTESIAN_POINT('Ctrl Pts',(15.1,0.469600118414825,3.7914923521806));
#14593=CARTESIAN_POINT('Ctrl Pts',(15.1,0.468037922355437,3.77755218535593));
#14594=CARTESIAN_POINT('Ctrl Pts',(15.1,0.467305764617198,3.77101881782393));
#14595=CARTESIAN_POINT('Ctrl Pts',(15.1,0.466444065557791,3.76449770946228));
#14596=CARTESIAN_POINT('Ctrl Pts',(15.1,0.465455885979624,3.7580011302485));
#14597=CARTESIAN_POINT('Ctrl Pts',(15.1,0.462059294618766,3.73567095330476));
#14598=CARTESIAN_POINT('Ctrl Pts',(15.1,0.45716703427379,3.71360451488159));
#14599=CARTESIAN_POINT('Ctrl Pts',(15.1,0.450855318277529,3.69195899424001));
#14600=CARTESIAN_POINT('Ctrl Pts',(15.1,0.444011336009419,3.66848810937402));
#14601=CARTESIAN_POINT('Ctrl Pts',(15.1,0.435499564516811,3.64551127788848));
#14602=CARTESIAN_POINT('Ctrl Pts',(15.1,0.425460105602329,3.62314791088594));
#14603=CARTESIAN_POINT('Ctrl Pts',(15.1,0.421555366121865,3.61444992000866));
#14604=CARTESIAN_POINT('Ctrl Pts',(15.1,0.417417266816347,3.60584160863805));
#14605=CARTESIAN_POINT('Ctrl Pts',(15.1,0.413065612826793,3.5973533346642));
#14606=CARTESIAN_POINT('Ctrl Pts',(15.1,0.400188909388694,3.57223622128044));
#14607=CARTESIAN_POINT('Ctrl Pts',(15.1,0.385429835973237,3.54813135585314));
#14608=CARTESIAN_POINT('Ctrl Pts',(15.1,0.369010648251791,3.52520488756047));
#14609=CARTESIAN_POINT('Ctrl Pts',(15.1,0.352591460530346,3.50227841926781));
#14610=CARTESIAN_POINT('Ctrl Pts',(15.1,0.334512091502091,3.48052876229398));
#14611=CARTESIAN_POINT('Ctrl Pts',(15.1,0.31493781544227,3.46010549098216));
#14612=CARTESIAN_POINT('Ctrl Pts',(14.8800042915148,-1.01702808208336E-5,
4.45785711824254));
#14613=CARTESIAN_POINT('Ctrl Pts',(14.8824938458936,-0.0238866377941533,
4.45787702641871));
#14614=CARTESIAN_POINT('Ctrl Pts',(14.8849834002724,-0.0477600743578134,
4.45604121816599));
#14615=CARTESIAN_POINT('Ctrl Pts',(14.8874729546512,-0.0713366221418418,
4.45232291776013));
#14616=CARTESIAN_POINT('Ctrl Pts',(14.8953443267012,-0.145879994579315,
4.44056654636394));
#14617=CARTESIAN_POINT('Ctrl Pts',(14.9032156987511,-0.217455452203791,
4.40999142286264));
#14618=CARTESIAN_POINT('Ctrl Pts',(14.9110870708011,-0.277486158769077,
4.36426138680722));
#14619=CARTESIAN_POINT('Ctrl Pts',(14.918958442851,-0.337516865334364,4.31853135075179));
#14620=CARTESIAN_POINT('Ctrl Pts',(14.926829814901,-0.38600282084046,4.25764640214225));
#14621=CARTESIAN_POINT('Ctrl Pts',(14.9347011869509,-0.417134151141141,
4.18890214416703));
#14622=CARTESIAN_POINT('Ctrl Pts',(14.9425725590009,-0.448265481441821,
4.12015788619182));
#14623=CARTESIAN_POINT('Ctrl Pts',(14.9504439310508,-0.462042186537087,
4.04355431885095));
#14624=CARTESIAN_POINT('Ctrl Pts',(14.9583153031008,-0.456813159708701,
3.96827104766458));
#14625=CARTESIAN_POINT('Ctrl Pts',(14.9661866751508,-0.451584132880315,
3.89298777647821));
#14626=CARTESIAN_POINT('Ctrl Pts',(14.9740580472007,-0.427349374128277,
3.81902480144635));
#14627=CARTESIAN_POINT('Ctrl Pts',(14.9819294192507,-0.387013471142241,
3.7552443159279));
#14628=CARTESIAN_POINT('Ctrl Pts',(14.9898007913006,-0.346677568156205,
3.69146383040944));
#14629=CARTESIAN_POINT('Ctrl Pts',(14.9976721633506,-0.290240520936171,
3.63786583440439));
#14630=CARTESIAN_POINT('Ctrl Pts',(15.0055435354005,-0.224463896228013,
3.60087434715852));
#14631=CARTESIAN_POINT('Ctrl Pts',(15.0134149074505,-0.158687271519854,
3.56388285991266));
#14632=CARTESIAN_POINT('Ctrl Pts',(15.0212862795004,-0.0835710693235713,
3.54349788142598));
#14633=CARTESIAN_POINT('Ctrl Pts',(15.0291576515504,-0.00811907658734153,
3.54215900695692));
#14634=CARTESIAN_POINT('Ctrl Pts',(15.0370290236004,0.067332916148885,3.54082013248786));
#14635=CARTESIAN_POINT('Ctrl Pts',(15.0449003956503,0.143120699425059,3.55852736203643));
#14636=CARTESIAN_POINT('Ctrl Pts',(15.0527717677003,0.210167800325704,3.59316557823286));
#14637=CARTESIAN_POINT('Ctrl Pts',(15.0606431397502,0.27721490122635,3.62780379442929));
#14638=CARTESIAN_POINT('Ctrl Pts',(15.0685145118002,0.335521319751467,3.67937299727358));
#14639=CARTESIAN_POINT('Ctrl Pts',(15.0763858838501,0.378083948355844,3.74167908197646));
#14640=CARTESIAN_POINT('Ctrl Pts',(15.0842572559001,0.420646576960222,3.80398516667934));
#14641=CARTESIAN_POINT('Ctrl Pts',(15.09212862795,0.447465415643859,3.87702813324079));
#14642=CARTESIAN_POINT('Ctrl Pts',(15.1,0.455362409197302,3.95209810113337));
#14643=CARTESIAN_POINT('Ctrl Pts',(12.5,0.310062960217722,4.54266560670548));
#14644=CARTESIAN_POINT('Ctrl Pts',(12.5,0.283442099593322,4.54921865641189));
#14645=CARTESIAN_POINT('Ctrl Pts',(12.5,0.256466577744696,4.55390832200786));
#14646=CARTESIAN_POINT('Ctrl Pts',(12.5,0.229324391633413,4.55669460918752));
#14647=CARTESIAN_POINT('Ctrl Pts',(12.5,0.202804350211112,4.55941702996513));
#14648=CARTESIAN_POINT('Ctrl Pts',(12.5,0.176124140498118,4.56032157710196));
#14649=CARTESIAN_POINT('Ctrl Pts',(12.5,0.149491279718871,4.55933465732487));
#14650=CARTESIAN_POINT('Ctrl Pts',(12.5,0.131604301980395,4.55867182909064));
#14651=CARTESIAN_POINT('Ctrl Pts',(12.5,0.113739373486447,4.5571550748263));
#14652=CARTESIAN_POINT('Ctrl Pts',(12.5,0.0959711573489174,4.5547553284502));
#14653=CARTESIAN_POINT('Ctrl Pts',(12.5,0.0885102514788159,4.55374767063663));
#14654=CARTESIAN_POINT('Ctrl Pts',(12.5,0.0810658284660142,4.55258395860043));
#14655=CARTESIAN_POINT('Ctrl Pts',(12.5,0.0736590895785168,4.55126509319275));
#14656=CARTESIAN_POINT('Ctrl Pts',(12.5,0.0532014046082737,4.54762233847462));
#14657=CARTESIAN_POINT('Ctrl Pts',(12.5,0.0329999615976937,4.54279338637244));
#14658=CARTESIAN_POINT('Ctrl Pts',(12.5,0.0131662989716721,4.53674486487483));
#14659=CARTESIAN_POINT('Ctrl Pts',(12.5,-0.00550403753485725,4.53105111411095));
#14660=CARTESIAN_POINT('Ctrl Pts',(12.5,-0.0238485481480196,4.52427602479051));
#14661=CARTESIAN_POINT('Ctrl Pts',(12.5,-0.0417515783368052,4.51643454453567));
#14662=CARTESIAN_POINT('Ctrl Pts',(12.5,-0.0500477299146631,4.51280085190917));
#14663=CARTESIAN_POINT('Ctrl Pts',(12.5,-0.058248775177811,4.50893813195896));
#14664=CARTESIAN_POINT('Ctrl Pts',(12.5,-0.0663415323109863,4.50484786558969));
#14665=CARTESIAN_POINT('Ctrl Pts',(12.5,-0.0727048112135971,4.50163171746301));
#14666=CARTESIAN_POINT('Ctrl Pts',(12.5,-0.0789919703630761,4.49827952355299));
#14667=CARTESIAN_POINT('Ctrl Pts',(12.5,-0.085197598682301,4.4947927546146));
#14668=CARTESIAN_POINT('Ctrl Pts',(12.5,-0.104491803581693,4.48395188067351));
#14669=CARTESIAN_POINT('Ctrl Pts',(12.5,-0.123002674071495,4.47180959856144));
#14670=CARTESIAN_POINT('Ctrl Pts',(12.5,-0.140547257611399,4.45840101528927));
#14671=CARTESIAN_POINT('Ctrl Pts',(12.5,-0.156644205929787,4.44609879839914));
#14672=CARTESIAN_POINT('Ctrl Pts',(12.5,-0.17192740174072,4.43272977950413));
#14673=CARTESIAN_POINT('Ctrl Pts',(12.5,-0.186217277007305,4.41832740439832));
#14674=CARTESIAN_POINT('Origin',(15.1,0.,4.));
#14675=CARTESIAN_POINT('',(15.1,-1.16619037896906,2.5));
#14676=CARTESIAN_POINT('',(15.1,1.16619037896906,2.5));
#14677=CARTESIAN_POINT('',(15.1,1.25,2.5));
#14678=CARTESIAN_POINT('Origin',(15.1,0.,4.));
#14679=CARTESIAN_POINT('Origin',(15.1,0.,4.));
#14680=CARTESIAN_POINT('',(15.1,2.75545529808154E-17,5.725));
#14681=CARTESIAN_POINT('Origin',(15.1,0.,5.5));
#14682=CARTESIAN_POINT('',(15.1,1.5,4.225));
#14683=CARTESIAN_POINT('Origin',(15.1,1.5,4.));
#14684=CARTESIAN_POINT('',(15.1,-1.5,4.225));
#14685=CARTESIAN_POINT('Origin',(15.1,-1.5,4.));
#14686=CARTESIAN_POINT('Origin',(14.4,-1.5,4.));
#14687=CARTESIAN_POINT('',(14.5,-1.5,4.225));
#14688=CARTESIAN_POINT('Origin',(14.5,-1.5,4.));
#14689=CARTESIAN_POINT('',(14.4,-1.5,4.225));
#14690=CARTESIAN_POINT('Origin',(14.4,1.5,4.));
#14691=CARTESIAN_POINT('',(14.5,1.5,4.225));
#14692=CARTESIAN_POINT('Origin',(14.5,1.5,4.));
#14693=CARTESIAN_POINT('',(14.4,1.5,4.225));
#14694=CARTESIAN_POINT('Origin',(14.4,0.,5.5));
#14695=CARTESIAN_POINT('',(14.5,-2.75545529808154E-17,5.725));
#14696=CARTESIAN_POINT('Origin',(14.5,0.,5.5));
#14697=CARTESIAN_POINT('',(14.4,-2.75545529808154E-17,5.725));
#14698=CARTESIAN_POINT('Origin',(14.4,2.5,2.5));
#14699=CARTESIAN_POINT('',(14.5,1.16619037896906,2.5));
#14700=CARTESIAN_POINT('',(14.5,-1.16619037896906,2.5));
#14701=CARTESIAN_POINT('',(14.5,1.25,2.5));
#14702=CARTESIAN_POINT('',(14.5,1.16619037896906,2.5));
#14703=CARTESIAN_POINT('',(14.5,-1.16619037896906,2.5));
#14704=CARTESIAN_POINT('Origin',(14.5,0.,4.));
#14705=CARTESIAN_POINT('Origin',(14.5,0.,4.));
#14706=CARTESIAN_POINT('',(14.5,-1.34711147906209E-16,5.1));
#14707=CARTESIAN_POINT('Origin',(14.5,0.,4.));
#14708=CARTESIAN_POINT('Origin',(14.5,0.,4.));
#14709=CARTESIAN_POINT('Origin',(12.5,0.,4.));
#14710=CARTESIAN_POINT('Origin',(12.5,0.,4.));
#14711=CARTESIAN_POINT('',(12.5,-1.34711147906209E-16,5.1));
#14712=CARTESIAN_POINT('',(12.5,-1.34711147906209E-16,5.1));
#14713=CARTESIAN_POINT('Origin',(12.5,0.,4.));
#14714=CARTESIAN_POINT('Origin',(12.5,0.,4.));
#25026=UNCERTAINTY_MEASURE_WITH_UNIT(LENGTH_MEASURE(0.001),#25075,
'DISTANCE_ACCURACY_VALUE',
'Maximum model space distance between geometric entities at asserted c
onnectivities');
#25040=UNCERTAINTY_MEASURE_WITH_UNIT(LENGTH_MEASURE(0.001),#25075,
'DISTANCE_ACCURACY_VALUE',
'Maximum model space distance between geometric entities at asserted c
onnectivities');
#25060=(
GEOMETRIC_REPRESENTATION_CONTEXT(3)
GLOBAL_UNCERTAINTY_ASSIGNED_CONTEXT((#25026))
GLOBAL_UNIT_ASSIGNED_CONTEXT((#25075,#25077,#25078))
REPRESENTATION_CONTEXT('','3D')
);
#25074=(
GEOMETRIC_REPRESENTATION_CONTEXT(3)
GLOBAL_UNCERTAINTY_ASSIGNED_CONTEXT((#25040))
GLOBAL_UNIT_ASSIGNED_CONTEXT((#25075,#25077,#25078))
REPRESENTATION_CONTEXT('','3D')
);
#25075=(
LENGTH_UNIT()
NAMED_UNIT(*)
SI_UNIT(.CENTI.,.METRE.)
);
#25077=(
NAMED_UNIT(*)
PLANE_ANGLE_UNIT()
SI_UNIT($,.RADIAN.)
);
#25078=(
NAMED_UNIT(*)
SI_UNIT($,.STERADIAN.)
SOLID_ANGLE_UNIT()
);
#25098=SHAPE_DEFINITION_REPRESENTATION(#25136,#25213);
#25136=PRODUCT_DEFINITION_SHAPE('',$,#25247);
#25213=SHAPE_REPRESENTATION('',(#8783),#25060);
#25227=PRODUCT_DEFINITION_CONTEXT('part definition',#25328,'design');
#25247=PRODUCT_DEFINITION('Flanged lead nut','Flanged lead nut',#25280,
#25227);
#25280=PRODUCT_DEFINITION_FORMATION('',$,#25349);
#25328=APPLICATION_CONTEXT(
'Core Data for Automotive Mechanical Design Process');
#25329=PRODUCT_CONTEXT('part definition',#25328,'mechanical');
#25349=PRODUCT('Flanged lead nut','Flanged lead nut','Flanged lead nut',
(#25329));
#25440=COLOUR_RGB('Black',0.12,0.14,0.17);
#25441=FILL_AREA_STYLE_COLOUR('',#25440);
#25442=FILL_AREA_STYLE('',(#25441));
#25443=SURFACE_STYLE_FILL_AREA(#25442);
#25444=SURFACE_SIDE_STYLE('',(#25443));
#25445=SURFACE_STYLE_USAGE(.BOTH.,#25444);
#25446=PRESENTATION_STYLE_ASSIGNMENT((#25445));
ENDSEC;
END-ISO-10303-21;
